ISO-10303-21;
HEADER;
FILE_DESCRIPTION (('STEP AP214'),
    '1' );
FILE_NAME ('Latch Bolt Assembly.step',
    '2026-10-06T13:23:30',
    ( '' ),
    ( '' ),
    'SwSTEP 2.0',
    'SolidWorks 2020',
    '' );
FILE_SCHEMA (( 'AUTOMOTIVE_DESIGN' ));
ENDSEC;

DATA;
#4=CARTESIAN_POINT ( 'NONE',  ( -30.49999999990000177, 47.50000000000000000, -147.5552959529999839 ) ) ;
#15=VECTOR ( 'NONE', #22356, 1000.000000000000000 ) ;
#38=CARTESIAN_POINT ( 'NONE',  ( 7.263251615191055777, 37.84880977052021223, -141.7037997430943790 ) ) ;
#53=DIRECTION ( 'NONE',  ( 1.000000000000000000, 0.000000000000000000, 0.000000000000000000 ) ) ;
#91=CARTESIAN_POINT ( 'NONE',  ( 9.327001754561790037, 35.74856537270147783, -141.8910607813375009 ) ) ;
#153=CARTESIAN_POINT ( 'NONE',  ( 8.154916571317706087, 35.54018629028437459, -142.0257885890718512 ) ) ;
#190=DIRECTION ( 'NONE',  ( -2.257039000139999987E-12, 0.000000000000000000, -1.000000000000000000 ) ) ;
#205=ORIENTED_EDGE ( 'NONE', *, *, #17674, .T. ) ;
#227=VECTOR ( 'NONE', #9869, 1000.000000000000000 ) ;
#230=CARTESIAN_POINT ( 'NONE',  ( 9.034463386642046956, 35.59814294577384430, -146.1252975212060505 ) ) ;
#271=CIRCLE ( 'NONE', #1413, 2.000000000000001776 ) ;
#280=ORIENTED_EDGE ( 'NONE', *, *, #14964, .T. ) ;
#283=DIRECTION ( 'NONE',  ( 2.602084747549999882E-17, -1.000000000000000000, -5.873289694040000105E-29 ) ) ;
#304=LINE ( 'NONE', #18742, #12898 ) ;
#311=CARTESIAN_POINT ( 'NONE',  ( 9.886079879350434751, 37.57350691547503629, -141.6219378633946917 ) ) ;
#315=AXIS2_PLACEMENT_3D ( 'NONE', #12975, #16085, #23342 ) ;
#372=DIRECTION ( 'NONE',  ( 0.000000000000000000, -1.000000000000000000, 0.000000000000000000 ) ) ;
#380=DIRECTION ( 'NONE',  ( 0.000000000000000000, 1.000000000000000000, 0.000000000000000000 ) ) ;
#383=CARTESIAN_POINT ( 'NONE',  ( 7.660612262366659486, 35.75684693635999878, -141.8862908784325612 ) ) ;
#429=FACE_OUTER_BOUND ( 'NONE', #6250, .T. ) ;
#433=CARTESIAN_POINT ( 'NONE',  ( 9.756656435460874022, 37.81905845387217369, -141.6932697408578576 ) ) ;
#484=ORIENTED_EDGE ( 'NONE', *, *, #15490, .T. ) ;
#504=CARTESIAN_POINT ( 'NONE',  ( 7.911979894106841549, 35.62004518156074795, -141.9706744367260853 ) ) ;
#526=LINE ( 'NONE', #3858, #17814 ) ;
#538=SHAPE_REPRESENTATION ( 'Latch Bolt Assembly', ( #5025 ), #7334 ) ;
#551=EDGE_CURVE ( 'NONE', #19314, #16041, #18247, .T. ) ;
#553=CARTESIAN_POINT ( 'NONE',  ( 9.088020105981311048, 38.37995481845652535, -141.9706744367346118 ) ) ;
#607=CARTESIAN_POINT ( 'NONE',  ( -30.49999999990000177, 29.00000000000000000, -147.5552959529999839 ) ) ;
#614=CARTESIAN_POINT ( 'NONE',  ( 7.393053867465662954, 35.98765375272272848, -141.7694449707084914 ) ) ;
#660=CARTESIAN_POINT ( 'NONE',  ( 8.914847504438609960, 38.44170426491582049, -142.0128484171024752 ) ) ;
#695=CARTESIAN_POINT ( 'NONE',  ( 9.797496117245477976, 37.75936717763469375, -146.4386832613834599 ) ) ;
#719=AXIS2_PLACEMENT_3D ( 'NONE', #21200, #4887, #3113 ) ;
#755=DIRECTION ( 'NONE',  ( -2.257039000139999987E-12, 0.000000000000000000, -1.000000000000000000 ) ) ;
#790=CARTESIAN_POINT ( 'NONE',  ( 8.013182962905725404, 38.41915155171203367, -146.1134792699380114 ) ) ;
#798=DIRECTION ( 'NONE',  ( -1.000000000000000000, 0.000000000000000000, 2.258108725280000263E-12 ) ) ;
#864=CARTESIAN_POINT ( 'NONE',  ( -46.50000000000000000, 37.00000000000000000, -148.4460207619999892 ) ) ;
#896=VERTEX_POINT ( 'NONE', #3343 ) ;
#908=CARTESIAN_POINT ( 'NONE',  ( 7.138086557144586841, 37.63063951478724078, -146.4749235844574002 ) ) ;
#932=CARTESIAN_POINT ( 'NONE',  ( 9.900763825459462097, 37.53873760029328821, -146.4970002627086956 ) ) ;
#967=DIRECTION ( 'NONE',  ( 1.000000000000000000, 0.000000000000000000, 0.000000000000000000 ) ) ;
#990=VERTEX_POINT ( 'NONE', #9815 ) ;
#1006=EDGE_CURVE ( 'NONE', #990, #7716, #8150, .T. ) ;
#1013=VECTOR ( 'NONE', #17401, 1000.000000000000000 ) ;
#1014=FACE_OUTER_BOUND ( 'NONE', #19027, .T. ) ;
#1032=ORIENTED_EDGE ( 'NONE', *, *, #12890, .T. ) ;
#1067=PRESENTATION_STYLE_ASSIGNMENT (( #2966 ) ) ;
#1074=PRODUCT_DEFINITION ( 'UNKNOWN', '', #13416, #3518 ) ;
#1086=FACE_OUTER_BOUND ( 'NONE', #5557, .T. ) ;
#1100=CARTESIAN_POINT ( 'NONE',  ( 14.50000000010000001, 37.00000000000000000, -144.0552959529999839 ) ) ;
#1103=LINE ( 'NONE', #6560, #18040 ) ;
#1124=CARTESIAN_POINT ( 'NONE',  ( 8.450744908290142021, 38.50000000000001421, -142.0552959529998702 ) ) ;
#1141=VECTOR ( 'NONE', #22229, 1000.000000000000000 ) ;
#1148=CARTESIAN_POINT ( 'NONE',  ( 7.310213413902445723, 37.91900551518246232, -146.3817958922534217 ) ) ;
#1161=DIRECTION ( 'NONE',  ( 1.000000000000000000, 0.000000000000000000, 0.000000000000000000 ) ) ;
#1189=AXIS2_PLACEMENT_3D ( 'NONE', #19887, #9150, #19642 ) ;
#1198=( LENGTH_UNIT ( ) NAMED_UNIT ( * ) SI_UNIT ( .MILLI., .METRE. ) );
#1227=DIRECTION ( 'NONE',  ( 1.734728570689999873E-18, 1.000000000000000000, 0.000000000000000000 ) ) ;
#1257=DIRECTION ( 'NONE',  ( -2.602084747549999882E-17, 1.000000000000000000, 5.873624107189999522E-29 ) ) ;
#1295=ORIENTED_EDGE ( 'NONE', *, *, #21347, .T. ) ;
#1298=DIRECTION ( 'NONE',  ( -2.250785033110000127E-12, 0.000000000000000000, -1.000000000000000000 ) ) ;
#1305=CARTESIAN_POINT ( 'NONE',  ( 8.302653104916485560, 38.49041384248582176, -146.0625927866742870 ) ) ;
#1333=ORIENTED_EDGE ( 'NONE', *, *, #4730, .T. ) ;
#1351=CARTESIAN_POINT ( 'NONE',  ( 7.073008394724321413, 36.53702466590743114, -141.5985056069079633 ) ) ;
#1395=PLANE ( 'NONE',  #13593 ) ;
#1399=CARTESIAN_POINT ( 'NONE',  ( 9.693958997696052293, 36.09174344073587548, -141.7260982849746540 ) ) ;
#1403=DIRECTION ( 'NONE',  ( -1.000000000000000000, 0.000000000000000000, 2.257076750620000196E-12 ) ) ;
#1413=AXIS2_PLACEMENT_3D ( 'NONE', #13472, #17045, #4794 ) ;
#1449=LINE ( 'NONE', #5365, #8779 ) ;
#1471=CARTESIAN_POINT ( 'NONE',  ( 7.209217092486989387, 36.23514394621652457, -141.6749984785230936 ) ) ;
#1472=ORIENTED_EDGE ( 'NONE', *, *, #18009, .T. ) ;
#1483=DIRECTION ( 'NONE',  ( -1.000000000000000000, 0.000000000000000000, 2.262079412673754432E-12 ) ) ;
#1498=EDGE_CURVE ( 'NONE', #11714, #23177, #21472, .T. ) ;
#1528=CARTESIAN_POINT ( 'NONE',  ( 9.488686602576935414, 35.87182884379176784, -141.8241438738831732 ) ) ;
#1538=CARTESIAN_POINT ( 'NONE',  ( -30.49999999990000177, 26.50000000000000000, -140.5552959529999839 ) ) ;
#1586=ORIENTED_EDGE ( 'NONE', *, *, #10056, .F. ) ;
#1597=CARTESIAN_POINT ( 'NONE',  ( 7.466903260932848951, 38.08760507689758157, -141.8042231706027394 ) ) ;
#1647=ORIENTED_EDGE ( 'NONE', *, *, #21592, .F. ) ;
#1648=CARTESIAN_POINT ( 'NONE',  ( 9.738534063751803416, 36.15378715822735955, -141.7028596377058705 ) ) ;
#1663=ORIENTED_EDGE ( 'NONE', *, *, #22844, .F. ) ;
#1667=CARTESIAN_POINT ( 'NONE',  ( -38.72222222220000276, 46.25000000000000000, -140.5552959529999839 ) ) ;
#1678=DIRECTION ( 'NONE',  ( -1.000000000000000000, 0.000000000000000000, 2.257171095940000041E-12 ) ) ;
#1684=DIRECTION ( 'NONE',  ( -1.000000000000000000, 0.000000000000000000, 2.257221436789999912E-12 ) ) ;
#1702=ORIENTED_EDGE ( 'NONE', *, *, #11680, .T. ) ;
#1709=CARTESIAN_POINT ( 'NONE',  ( 7.719632372826509048, 38.28109096042884119, -141.9084521925880154 ) ) ;
#1722=ORIENTED_EDGE ( 'NONE', *, *, #4603, .T. ) ;
#1723=DIRECTION ( 'NONE',  ( -1.000000000000000000, 1.734728570689999873E-18, 2.257171095940000041E-12 ) ) ;
#1759=CARTESIAN_POINT ( 'NONE',  ( 9.297187311559401479, 35.72924951987560149, -141.9023098457803940 ) ) ;
#1790=DIRECTION ( 'NONE',  ( -2.257171095940000041E-12, -1.003664318210000046E-28, -1.000000000000000000 ) ) ;
#1791=PLANE ( 'NONE',  #4808 ) ;
#1796=CARTESIAN_POINT ( 'NONE',  ( -31.00000000000000000, 47.50000000000000000, -149.5552959529999839 ) ) ;
#1804=DIRECTION ( 'NONE',  ( 2.257157423930000049E-12, 0.000000000000000000, 1.000000000000000000 ) ) ;
#1823=CARTESIAN_POINT ( 'NONE',  ( 7.879765099526474081, 38.36639659745271302, -141.9617131063228328 ) ) ;
#1877=CARTESIAN_POINT ( 'NONE',  ( 8.673959633207795505, 35.50990985248334653, -142.0478861723181581 ) ) ;
#1901=LINE ( 'NONE', #1667, #8045 ) ;
#1967=LINE ( 'NONE', #18260, #3295 ) ;
#1973=EDGE_CURVE ( 'NONE', #18574, #11235, #9120, .T. ) ;
#2001=CARTESIAN_POINT ( 'NONE',  ( 9.949375129378253746, 37.38976472558845643, -141.5855402290607685 ) ) ;
#2017=DIRECTION ( 'NONE',  ( -2.602084747549999882E-17, 1.000000000000000000, 5.873289694040000105E-29 ) ) ;
#2019=PRODUCT_CONTEXT ( 'NONE', #20893, 'mechanical' ) ;
#2058=CARTESIAN_POINT ( 'NONE',  ( -46.00000000000000000, 37.00000000000000000, -149.5552959529999839 ) ) ;
#2061=CARTESIAN_POINT ( 'NONE',  ( 7.643324914822369642, 35.76867410208022591, -141.8794674798148776 ) ) ;
#2080=CARTESIAN_POINT ( 'NONE',  ( -46.00000000000000000, 26.50000000000000000, -149.0552959529999839 ) ) ;
#2097=EDGE_LOOP ( 'NONE', ( #19263, #17599 ) ) ;
#2104=CARTESIAN_POINT ( 'NONE',  ( 8.811894473837091013, 38.46727147861445673, -142.0311810631515925 ) ) ;
#2116=ORIENTED_EDGE ( 'NONE', *, *, #8857, .F. ) ;
#2137=CARTESIAN_POINT ( 'NONE',  ( 8.842821505070592281, 35.53864366126496321, -146.0837389892870988 ) ) ;
#2172=CARTESIAN_POINT ( 'NONE',  ( 7.966339544912719894, 35.59716178443439105, -141.9858703028249067 ) ) ;
#2221=CARTESIAN_POINT ( 'NONE',  ( 9.809232433496585912, 37.73246533773845357, -141.6649243764299797 ) ) ;
#2228=STYLED_ITEM ( 'NONE', ( #4378 ), #20016 ) ;
#2274=AXIS2_PLACEMENT_3D ( 'NONE', #1100, #20972, #1227 ) ;
#2297=CARTESIAN_POINT ( 'NONE',  ( 7.651143207404245139, 35.76327648575674090, -141.8825763915462517 ) ) ;
#2308=CARTESIAN_POINT ( 'NONE',  ( -30.49999999990000177, 46.25000000000000000, -147.5552959529999839 ) ) ;
#2340=AXIS2_PLACEMENT_3D ( 'NONE', #10063, #10187, #20801 ) ;
#2344=CARTESIAN_POINT ( 'NONE',  ( 9.593201079431377565, 38.02725237339706155, -141.7760678466342767 ) ) ;
#2357=ORIENTED_EDGE ( 'NONE', *, *, #18288, .F. ) ;
#2376=CARTESIAN_POINT ( 'NONE',  ( -30.49999999990000177, 26.50000000000000000, -139.8052959529999839 ) ) ;
#2412=CARTESIAN_POINT ( 'NONE',  ( 7.898597776409067350, 35.62582981816382954, -141.9668508539811285 ) ) ;
#2423=DIRECTION ( 'NONE',  ( 0.000000000000000000, 1.000000000000000000, 0.000000000000000000 ) ) ;
#2431=EDGE_LOOP ( 'NONE', ( #1647, #10781 ) ) ;
#2456=CARTESIAN_POINT ( 'NONE',  ( 9.695206431619142862, 37.90762969977967600, -141.7255920984417514 ) ) ;
#2457=CARTESIAN_POINT ( 'NONE',  ( 7.310162460357136460, 36.08106663428162619, -146.3818244917397635 ) ) ;
#2468=DIRECTION ( 'NONE',  ( 0.000000000000000000, 1.000000000000000000, 0.000000000000000000 ) ) ;
#2482=ADVANCED_FACE ( 'NONE', ( #20760 ), #7663, .T. ) ;
#2501=ORIENTED_EDGE ( 'NONE', *, *, #6823, .T. ) ;
#2570=CARTESIAN_POINT ( 'NONE',  ( 7.204510097230632404, 37.75811448146659188, -146.4379907056525951 ) ) ;
#2612=SHAPE_REPRESENTATION_RELATIONSHIP ( 'NONE' , 'NONE' ,  #538, #22005 ) ;
#2641=DIRECTION ( 'NONE',  ( -2.257157423930000049E-12, 0.000000000000000000, -1.000000000000000000 ) ) ;
#2689=CARTESIAN_POINT ( 'NONE',  ( 7.202503882904777832, 36.24063282234246230, -146.4386832613703575 ) ) ;
#2695=ADVANCED_FACE ( 'NONE', ( #1014 ), #8590, .T. ) ;
#2718=CARTESIAN_POINT ( 'NONE',  ( 9.948241962799819760, 37.39437665988412363, -146.5244709269353791 ) ) ;
#2721=ORIENTED_EDGE ( 'NONE', *, *, #8082, .T. ) ;
#2726=CYLINDRICAL_SURFACE ( 'NONE', #2340, 0.5000000000000004441 ) ;
#2731=CARTESIAN_POINT ( 'NONE',  ( -38.50000000000000000, 47.50000000000000000, -149.5552959529999839 ) ) ;
#2737=( NAMED_UNIT ( * ) SI_UNIT ( $, .STERADIAN. ) SOLID_ANGLE_UNIT ( ) );
#2778=LINE ( 'NONE', #8813, #4152 ) ;
#2779=EDGE_LOOP ( 'NONE', ( #13040, #10289, #13027, #20220, #7821, #18203, #16899 ) ) ;
#2811=CARTESIAN_POINT ( 'NONE',  ( -38.72222222220000276, 29.00000000000000000, -140.5552959529999839 ) ) ;
#2827=CARTESIAN_POINT ( 'NONE',  ( 9.629496873833184978, 37.99207690572956153, -146.3513483205671832 ) ) ;
#2886=DIRECTION ( 'NONE',  ( 0.000000000000000000, -1.000000000000000000, -2.341876234024414612E-17 ) ) ;
#2919=CARTESIAN_POINT ( 'NONE',  ( 6.999993628236942378, 36.89957845934668512, -146.5552973561658803 ) ) ;
#2947=CARTESIAN_POINT ( 'NONE',  ( 9.125765718317245145, 38.36348339572941057, -146.1507818850132026 ) ) ;
#2952=FACE_OUTER_BOUND ( 'NONE', #9670, .T. ) ;
#2963=APPLICATION_CONTEXT ( 'automotive_design' ) ;
#2965=ORIENTED_EDGE ( 'NONE', *, *, #20292, .F. ) ;
#2966=SURFACE_STYLE_USAGE ( .BOTH. , #6176 ) ;
#3010=CARTESIAN_POINT ( 'NONE',  ( -30.99999999989999822, 47.50000000000000000, -138.5552959529999839 ) ) ;
#3024=PLANE ( 'NONE',  #11971 ) ;
#3113=DIRECTION ( 'NONE',  ( -0.6689647316207345540, 0.000000000000000000, 0.7432941462487100415 ) ) ;
#3127=ORIENTED_EDGE ( 'NONE', *, *, #10459, .F. ) ;
#3206=EDGE_CURVE ( 'NONE', #11665, #21515, #1103, .T. ) ;
#3242=CARTESIAN_POINT ( 'NONE',  ( 7.665856076347231429, 38.24667833328184230, -141.8883195129079979 ) ) ;
#3256=ORIENTED_EDGE ( 'NONE', *, *, #12141, .F. ) ;
#3294=CARTESIAN_POINT ( 'NONE',  ( 9.634600858332637685, 36.01766042586972816, -141.7561022817950800 ) ) ;
#3295=VECTOR ( 'NONE', #5631, 1000.000000000000000 ) ;
#3303=VECTOR ( 'NONE', #15149, 1000.000000000000000 ) ;
#3316=EDGE_LOOP ( 'NONE', ( #8032, #3427, #1295, #5835 ) ) ;
#3343=CARTESIAN_POINT ( 'NONE',  ( -30.49999999990282262, 39.50000000000000000, -144.0552959529548502 ) ) ;
#3356=CARTESIAN_POINT ( 'NONE',  ( 7.306041003437069747, 37.90825656058944304, -141.7260982854917017 ) ) ;
#3376=ORIENTED_EDGE ( 'NONE', *, *, #9089, .T. ) ;
#3427=ORIENTED_EDGE ( 'NONE', *, *, #8344, .F. ) ;
#3480=CARTESIAN_POINT ( 'NONE',  ( 7.942238981814500498, 38.39246003580940680, -141.9790531659411101 ) ) ;
#3518=PRODUCT_DEFINITION_CONTEXT ( 'detailed design', #2963, 'design' ) ;
#3535=CARTESIAN_POINT ( 'NONE',  ( 8.549255091327660594, 35.49999999999985789, -142.0552959530001260 ) ) ;
#3540=LINE ( 'NONE', #14360, #4176 ) ;
#3548=DIRECTION ( 'NONE',  ( -1.000000000000000000, 0.000000000000000000, 2.256683728769999802E-12 ) ) ;
#3588=EDGE_CURVE ( 'NONE', #7716, #16508, #21063, .T. ) ;
#3602=CARTESIAN_POINT ( 'NONE',  ( 7.228461998321116688, 37.79745240714011345, -141.6854458089358104 ) ) ;
#3650=CARTESIAN_POINT ( 'NONE',  ( 8.844715317520215336, 35.53941187169878191, -142.0263608017556010 ) ) ;
#3658=PLANE ( 'NONE',  #10935 ) ;
#3691=DIRECTION ( 'NONE',  ( 0.000000000000000000, 5.873289694040000105E-29, -1.000000000000000000 ) ) ;
#3713=CARTESIAN_POINT ( 'NONE',  ( 7.365399142987872239, 37.98233957550490913, -141.7561022823591657 ) ) ;
#3735=AXIS2_PLACEMENT_3D ( 'NONE', #8390, #21018, #19216 ) ;
#3747=UNCERTAINTY_MEASURE_WITH_UNIT (LENGTH_MEASURE( 1.000000000000000082E-05 ), #1198, 'distance_accuracy_value', 'NONE');
#3764=CARTESIAN_POINT ( 'NONE',  ( 9.556107899309107978, 35.93480091585412595, -141.7935801463470966 ) ) ;
#3811=AXIS2_PLACEMENT_3D ( 'NONE', #23132, #5151, #12400 ) ;
#3813=DIRECTION ( 'NONE',  ( 2.602084747549999882E-17, -1.000000000000000000, -5.873289694040000105E-29 ) ) ;
#3858=CARTESIAN_POINT ( 'NONE',  ( -38.39535039439999764, 45.00000000000000000, -147.5552959529999839 ) ) ;
#3890=CARTESIAN_POINT ( 'NONE',  ( 8.879708087000684813, 38.45148868343596860, -142.0197959584526188 ) ) ;
#3929=PLANE ( 'NONE',  #18704 ) ;
#3937=CARTESIAN_POINT ( 'NONE',  ( -10.49999999989999822, 39.50000000000000000, -144.0552959529999839 ) ) ;
#3940=ORIENTED_EDGE ( 'NONE', *, *, #14964, .F. ) ;
#3956=CARTESIAN_POINT ( 'NONE',  ( -46.50000000000000000, 26.50000000000000000, -148.4460207619999892 ) ) ;
#3958=CARTESIAN_POINT ( 'NONE',  ( -42.28007584270000052, 29.00000000000000000, -143.7573642109999810 ) ) ;
#3976=LINE ( 'NONE', #18731, #21949 ) ;
#3992=DIRECTION ( 'NONE',  ( 2.602084747549999882E-17, -1.000000000000000000, -5.873289694040000105E-29 ) ) ;
#3996=CARTESIAN_POINT ( 'NONE',  ( 9.990807518853022984, 37.19361385680454646, -141.5610522423011730 ) ) ;
#4018=ORIENTED_EDGE ( 'NONE', *, *, #12890, .F. ) ;
#4062=CARTESIAN_POINT ( 'NONE',  ( 7.436216203403632541, 35.94246666510559152, -141.7899860742952853 ) ) ;
#4078=VERTEX_POINT ( 'NONE', #20789 ) ;
#4081=CARTESIAN_POINT ( 'NONE',  ( -31.00000000000000000, 26.50000000000000000, -149.5552959529999839 ) ) ;
#4106=CARTESIAN_POINT ( 'NONE',  ( 9.356675081444274511, 38.23132590060392033, -141.8794674813294989 ) ) ;
#4111=CIRCLE ( 'NONE', #15900, 0.5000000000000004441 ) ;
#4142=AXIS2_PLACEMENT_3D ( 'NONE', #16291, #12466, #8775 ) ;
#4152=VECTOR ( 'NONE', #12381, 1000.000000000000000 ) ;
#4176=VECTOR ( 'NONE', #21751, 1000.000000000000000 ) ;
#4184=VECTOR ( 'NONE', #6760, 1000.000000000000000 ) ;
#4200=VERTEX_POINT ( 'NONE', #12554 ) ;
#4223=CARTESIAN_POINT ( 'NONE',  ( -30.49999999990000177, 47.50000000000000000, -147.5552959529999839 ) ) ;
#4233=CARTESIAN_POINT ( 'NONE',  ( 9.116160410115874413, 38.36768097678178435, -141.9625758178371484 ) ) ;
#4254=ADVANCED_FACE ( 'NONE', ( #12208 ), #1395, .T. ) ;
#4260=VECTOR ( 'NONE', #2468, 1000.000000000000000 ) ;
#4295=EDGE_CURVE ( 'NONE', #19783, #6756, #4111, .T. ) ;
#4371=LINE ( 'NONE', #9035, #23538 ) ;
#4378=PRESENTATION_STYLE_ASSIGNMENT (( #7936 ) ) ;
#4382=DIRECTION ( 'NONE',  ( 0.000000000000000000, 1.000000000000000000, 0.000000000000000000 ) ) ;
#4417=EDGE_CURVE ( 'NONE', #7697, #23331, #22730, .T. ) ;
#4427=ORIENTED_EDGE ( 'NONE', *, *, #8857, .T. ) ;
#4429=ADVANCED_FACE ( 'NONE', ( #429 ), #6216, .F. ) ;
#4462=CARTESIAN_POINT ( 'NONE',  ( 7.158503024131143810, 37.67301910471298498, -146.4634108040858678 ) ) ;
#4489=CARTESIAN_POINT ( 'NONE',  ( 9.999986723869190186, 36.79905214429372506, -146.5552931460613877 ) ) ;
#4500=ORIENTED_EDGE ( 'NONE', *, *, #4417, .T. ) ;
#4504=CIRCLE ( 'NONE', #315, 0.5000000000000004441 ) ;
#4515=EDGE_CURVE ( 'NONE', #7716, #22942, #12854, .T. ) ;
#4526=DIRECTION ( 'NONE',  ( 0.000000000000000000, 1.000000000000000000, 0.000000000000000000 ) ) ;
#4545=CIRCLE ( 'NONE', #18979, 2.000000000000001776 ) ;
#4559=CARTESIAN_POINT ( 'NONE',  ( -44.50000000000000000, 47.50000000000000000, -148.4460207619999892 ) ) ;
#4580=CARTESIAN_POINT ( 'NONE',  ( 7.830020039297265200, 38.34549836880493956, -146.1628100146799341 ) ) ;
#4590=CARTESIAN_POINT ( 'NONE',  ( 0.000000000000000000, 0.000000000000000000, 0.000000000000000000 ) ) ;
#4603=EDGE_CURVE ( 'NONE', #18727, #8753, #4504, .T. ) ;
#4612=CARTESIAN_POINT ( 'NONE',  ( 9.960568225534427000, 37.34605842341183291, -146.5317159311745741 ) ) ;
#4615=EDGE_LOOP ( 'NONE', ( #11689, #18052, #484, #17711 ) ) ;
#4700=CARTESIAN_POINT ( 'NONE',  ( 7.156500972566314012, 36.32574979380856206, -146.4644491674769426 ) ) ;
#4718=ADVANCED_FACE ( 'NONE', ( #7612 ), #22258, .T. ) ;
#4726=CARTESIAN_POINT ( 'NONE',  ( 9.412671590450063519, 35.80533467859499552, -146.2522312778014282 ) ) ;
#4730=EDGE_CURVE ( 'NONE', #21289, #8120, #9386, .T. ) ;
#4779=DIRECTION ( 'NONE',  ( 0.000000000000000000, -1.000000000000000000, 0.000000000000000000 ) ) ;
#4787=AXIS2_PLACEMENT_3D ( 'NONE', #1538, #21638, #8877 ) ;
#4794=DIRECTION ( 'NONE',  ( 1.000000000000000000, 0.000000000000000000, 0.000000000000000000 ) ) ;
#4808=AXIS2_PLACEMENT_3D ( 'NONE', #4, #12713, #11043 ) ;
#4820=DIRECTION ( 'NONE',  ( -1.000000000000000000, 0.000000000000000000, 2.257221436789999912E-12 ) ) ;
#4847=ORIENTED_EDGE ( 'NONE', *, *, #23519, .T. ) ;
#4862=( NAMED_UNIT ( * ) PLANE_ANGLE_UNIT ( ) SI_UNIT ( $, .RADIAN. ) );
#4887=DIRECTION ( 'NONE',  ( -2.602084747547159675E-17, 1.000000000000000000, 2.714790849608250461E-29 ) ) ;
#4905=CARTESIAN_POINT ( 'NONE',  ( 8.500000000060001781, 38.50000000000000000, -146.0552959529999839 ) ) ;
#4914=ORIENTED_EDGE ( 'NONE', *, *, #18272, .F. ) ;
#4920=CIRCLE ( 'NONE', #15939, 0.5000000000000004441 ) ;
#4945=CIRCLE ( 'NONE', #18252, 2.000000000000001776 ) ;
#4978=EDGE_LOOP ( 'NONE', ( #2501, #16403, #19719, #4427, #14728 ) ) ;
#5025=AXIS2_PLACEMENT_3D ( 'NONE', #4590, #17084, #1161 ) ;
#5033=DIRECTION ( 'NONE',  ( 0.000000000000000000, -1.000000000000000000, 0.000000000000000000 ) ) ;
#5034=CARTESIAN_POINT ( 'NONE',  ( 7.136768929676958528, 37.62588656037802082, -141.6348998444176743 ) ) ;
#5079=CARTESIAN_POINT ( 'NONE',  ( 9.346855175913132641, 35.76186543769073012, -141.8834125995852844 ) ) ;
#5086=DIRECTION ( 'NONE',  ( 1.000000000000000000, 0.000000000000000000, -2.257171095940000041E-12 ) ) ;
#5135=CARTESIAN_POINT ( 'NONE',  ( 7.255075146305371980, 36.16322928933654168, -141.6994869973446498 ) ) ;
#5151=DIRECTION ( 'NONE',  ( 2.257171095940000041E-12, 1.003664318209372040E-28, 1.000000000000000000 ) ) ;
#5175=DIRECTION ( 'NONE',  ( -1.000000000000000000, 0.000000000000000000, 2.257076750620000196E-12 ) ) ;
#5177=ORIENTED_EDGE ( 'NONE', *, *, #20846, .F. ) ;
#5190=CARTESIAN_POINT ( 'NONE',  ( 9.999995540850324716, 36.80846206152234856, -141.5553035006076072 ) ) ;
#5221=ORIENTED_EDGE ( 'NONE', *, *, #18484, .T. ) ;
#5233=ORIENTED_EDGE ( 'NONE', *, *, #3206, .F. ) ;
#5256=CARTESIAN_POINT ( 'NONE',  ( 7.167702963139642058, 37.68962278446276315, -141.6522196278403669 ) ) ;
#5365=CARTESIAN_POINT ( 'NONE',  ( -30.49999999990000177, 47.50000000000000000, -139.8052959529999839 ) ) ;
#5376=EDGE_CURVE ( 'NONE', #8910, #10616, #22961, .T. ) ;
#5383=CARTESIAN_POINT ( 'NONE',  ( 7.277539027747931932, 37.86935047857989645, -141.7113041814175745 ) ) ;
#5395=CARTESIAN_POINT ( 'NONE',  ( -30.49999999990000177, 27.75000000000000000, -140.5552959529999839 ) ) ;
#5401=CARTESIAN_POINT ( 'NONE',  ( -37.89633983739999934, 47.50000000000000000, -139.8120018070000015 ) ) ;
#5417=DIRECTION ( 'NONE',  ( 2.257157423930000049E-12, 0.000000000000000000, 1.000000000000000000 ) ) ;
#5437=CARTESIAN_POINT ( 'NONE',  ( 9.280367625918376717, 35.71890903872555612, -141.9084521930435017 ) ) ;
#5471=FACE_OUTER_BOUND ( 'NONE', #13086, .T. ) ;
#5479=DIRECTION ( 'NONE',  ( 1.000000000000000000, 2.602084704489999637E-17, -2.257171095940000041E-12 ) ) ;
#5499=CARTESIAN_POINT ( 'NONE',  ( 7.653144819507610386, 38.23813455914281434, -141.8834125977530221 ) ) ;
#5517=DIRECTION ( 'NONE',  ( -2.602084747549999882E-17, 1.000000000000000000, 5.873289694040000105E-29 ) ) ;
#5547=CARTESIAN_POINT ( 'NONE',  ( 8.962004831856564380, 35.57270853839675340, -142.0027968019423383 ) ) ;
#5557=EDGE_LOOP ( 'NONE', ( #18380, #23419, #10749, #10381 ) ) ;
#5561=CARTESIAN_POINT ( 'NONE',  ( 8.500000000060001781, 35.50000000000000000, -142.0552959529999839 ) ) ;
#5574=CARTESIAN_POINT ( 'NONE',  ( 8.500000000060001781, 35.50000000000000000, -146.0552959529999839 ) ) ;
#5575=EDGE_CURVE ( 'NONE', #13874, #990, #4920, .T. ) ;
#5587=LINE ( 'NONE', #12835, #12134 ) ;
#5590=EDGE_LOOP ( 'NONE', ( #9051, #8216 ) ) ;
#5631=DIRECTION ( 'NONE',  ( -1.000000000000000000, 0.000000000000000000, 2.257076750570000197E-12 ) ) ;
#5653=ORIENTED_EDGE ( 'NONE', *, *, #21592, .T. ) ;
#5655=CARTESIAN_POINT ( 'NONE',  ( 9.576259528318086467, 38.04486978495457095, -141.7841118833629821 ) ) ;
#5663=AXIS2_PLACEMENT_3D ( 'NONE', #17454, #6270, #20677 ) ;
#5689=CARTESIAN_POINT ( 'NONE',  ( 9.169979960837745026, 35.65450163122486771, -146.1628100147027567 ) ) ;
#5725=CARTESIAN_POINT ( 'NONE',  ( 7.908363834111431068, 35.62159694921923858, -141.9696471534852549 ) ) ;
#5752=EDGE_CURVE ( 'NONE', #10168, #13979, #2778, .T. ) ;
#5775=CARTESIAN_POINT ( 'NONE',  ( 8.822124130990804503, 38.46505108584880617, -142.0295714736415107 ) ) ;
#5789=ORIENTED_EDGE ( 'NONE', *, *, #13313, .T. ) ;
#5792=SHAPE_DEFINITION_REPRESENTATION ( #11883, #538 ) ;
#5814=( GEOMETRIC_REPRESENTATION_CONTEXT ( 3 ) GLOBAL_UNCERTAINTY_ASSIGNED_CONTEXT ( ( #3747 ) ) GLOBAL_UNIT_ASSIGNED_CONTEXT ( ( #1198, #4862, #21176 ) ) REPRESENTATION_CONTEXT ( 'NONE', 'WORKASPACE' ) );
#5835=ORIENTED_EDGE ( 'NONE', *, *, #13313, .F. ) ;
#5839=CARTESIAN_POINT ( 'NONE',  ( 7.662331531295155429, 35.75568826264862565, -141.8869580487122732 ) ) ;
#5851=ORIENTED_EDGE ( 'NONE', *, *, #23496, .F. ) ;
#5869=ORIENTED_EDGE ( 'NONE', *, *, #9089, .F. ) ;
#5887=CARTESIAN_POINT ( 'NONE',  ( 9.767209682567662199, 37.80278906969247288, -141.6876531319532546 ) ) ;
#5898=VERTEX_POINT ( 'NONE', #4905 ) ;
#5912=LINE ( 'NONE', #13167, #21379 ) ;
#5931=DIRECTION ( 'NONE',  ( 1.000000000000000000, 0.000000000000000000, -2.257171095940000041E-12 ) ) ;
#5954=CARTESIAN_POINT ( 'NONE',  ( 8.500000000060001781, 35.50000000000000000, -142.0552959529999839 ) ) ;
#5987=EDGE_CURVE ( 'NONE', #6638, #8120, #4371, .T. ) ;
#6001=AXIS2_PLACEMENT_3D ( 'NONE', #19607, #15797, #14251 ) ;
#6004=CARTESIAN_POINT ( 'NONE',  ( 9.606946132914400138, 38.01234624700477127, -141.7694449706205546 ) ) ;
#6019=AXIS2_PLACEMENT_3D ( 'NONE', #23427, #16173, #18073 ) ;
#6034=ORIENTED_EDGE ( 'NONE', *, *, #1973, .F. ) ;
#6049=VERTEX_POINT ( 'NONE', #6513 ) ;
#6055=CARTESIAN_POINT ( 'NONE',  ( -30.49999999990000177, 26.50000000000000000, -147.5552959529999839 ) ) ;
#6127=CARTESIAN_POINT ( 'NONE',  ( 9.348856789759086183, 38.23672351627273969, -141.8825763927054311 ) ) ;
#6128=EDGE_CURVE ( 'NONE', #22716, #990, #13889, .T. ) ;
#6159=CARTESIAN_POINT ( 'NONE',  ( 9.293598222543803189, 38.27417067585172816, -146.2064413145477317 ) ) ;
#6176=SURFACE_SIDE_STYLE ('',( #21057 ) ) ;
#6195=CARTESIAN_POINT ( 'NONE',  ( -30.49999999990000177, 37.00000000000000000, -144.0552959529999839 ) ) ;
#6216=PLANE ( 'NONE',  #12465 ) ;
#6232=EDGE_CURVE ( 'NONE', #21515, #21976, #3540, .T. ) ;
#6244=CARTESIAN_POINT ( 'NONE',  ( 7.810046034465172760, 35.66771806836383263, -146.1707627155566911 ) ) ;
#6250=EDGE_LOOP ( 'NONE', ( #1586, #15580, #1333, #8573, #17595, #8917, #5789, #22171 ) ) ;
#6270=DIRECTION ( 'NONE',  ( -2.602084747549999882E-17, 1.000000000000000000, 5.873289694040000105E-29 ) ) ;
#6305=FACE_OUTER_BOUND ( 'NONE', #16005, .T. ) ;
#6308=ORIENTED_EDGE ( 'NONE', *, *, #8344, .T. ) ;
#6311=EDGE_CURVE ( 'NONE', #19314, #9544, #17695, .T. ) ;
#6331=ORIENTED_EDGE ( 'NONE', *, *, #8469, .T. ) ;
#6359=CARTESIAN_POINT ( 'NONE',  ( 7.587222251655057370, 35.80541937760241922, -146.2522771197009206 ) ) ;
#6384=VECTOR ( 'NONE', #372, 1000.000000000000000 ) ;
#6386=CARTESIAN_POINT ( 'NONE',  ( 9.689786586155861414, 36.08099448470404980, -146.3817958922141429 ) ) ;
#6449=LINE ( 'NONE', #19300, #13326 ) ;
#6486=CARTESIAN_POINT ( 'NONE',  ( 7.039431774584924639, 36.65394157649679840, -146.5317159311551336 ) ) ;
#6512=CARTESIAN_POINT ( 'NONE',  ( 9.489186301925801814, 35.86813483702695038, -146.2857056571775729 ) ) ;
#6513=CARTESIAN_POINT ( 'NONE',  ( -46.29070078840000235, 26.50000000000000000, -147.5552959529999839 ) ) ;
#6560=CARTESIAN_POINT ( 'NONE',  ( -30.99999999989999822, 37.00000000000000000, -138.5552959529999839 ) ) ;
#6575=CARTESIAN_POINT ( 'NONE',  ( 8.326040366162002826, 38.49009014742802037, -142.0478861723179023 ) ) ;
#6638=VERTEX_POINT ( 'NONE', #13238 ) ;
#6642=FILL_AREA_STYLE_COLOUR ( '', #16827 ) ;
#6688=CARTESIAN_POINT ( 'NONE',  ( 8.108818582516752471, 38.44893568608949863, -142.0179551230363870 ) ) ;
#6723=EDGE_CURVE ( 'NONE', #6638, #21976, #271, .T. ) ;
#6742=AXIS2_PLACEMENT_3D ( 'NONE', #22612, #7969, #4526 ) ;
#6756=VERTEX_POINT ( 'NONE', #18730 ) ;
#6760=DIRECTION ( 'NONE',  ( 2.262447131730000305E-12, 0.000000000000000000, 1.000000000000000000 ) ) ;
#6764=EDGE_CURVE ( 'NONE', #9544, #16508, #17741, .T. ) ;
#6775=ORIENTED_EDGE ( 'NONE', *, *, #6764, .T. ) ;
#6803=CARTESIAN_POINT ( 'NONE',  ( -34.61111111099999960, 45.00000000000000000, -140.5552959529999839 ) ) ;
#6804=CARTESIAN_POINT ( 'NONE',  ( -30.49999999990000177, 45.00000000000000000, -147.5552959529999839 ) ) ;
#6806=CYLINDRICAL_SURFACE ( 'NONE', #14344, 2.500000000000002220 ) ;
#6807=CARTESIAN_POINT ( 'NONE',  ( 7.571119092374880566, 38.17802949123974798, -141.8499009779202140 ) ) ;
#6823=EDGE_CURVE ( 'NONE', #7697, #19038, #16931, .T. ) ;
#6849=ORIENTED_EDGE ( 'NONE', *, *, #14812, .F. ) ;
#6860=CARTESIAN_POINT ( 'NONE',  ( 9.722460972908612220, 36.13064952216455339, -141.7113041811295773 ) ) ;
#6904=AXIS2_PLACEMENT_3D ( 'NONE', #10569, #5479, #17731 ) ;
#6929=CARTESIAN_POINT ( 'NONE',  ( 6.999997771067969943, 36.90428341750195784, -141.5552923337224058 ) ) ;
#6981=CARTESIAN_POINT ( 'NONE',  ( 9.876586606239635913, 36.40403110125505037, -141.6273462229582947 ) ) ;
#6988=FACE_OUTER_BOUND ( 'NONE', #13081, .T. ) ;
#6989=ADVANCED_FACE ( 'NONE', ( #23115, #14425 ), #6806, .T. ) ;
#7021=ORIENTED_EDGE ( 'NONE', *, *, #22844, .T. ) ;
#7040=CARTESIAN_POINT ( 'NONE',  ( 7.960302519239492725, 38.39964962483306010, -141.9838786040258469 ) ) ;
#7059=CARTESIAN_POINT ( 'NONE',  ( -30.99999999989999822, 47.50000000000000000, -139.0552959529999839 ) ) ;
#7078=ORIENTED_EDGE ( 'NONE', *, *, #9306, .T. ) ;
#7082=ORIENTED_EDGE ( 'NONE', *, *, #8583, .F. ) ;
#7119=ORIENTED_EDGE ( 'NONE', *, *, #14942, .T. ) ;
#7148=ADVANCED_FACE ( 'NONE', ( #1086 ), #19158, .F. ) ;
#7160=CARTESIAN_POINT ( 'NONE',  ( 7.123413393902458424, 37.59596889877142445, -141.6273462229617621 ) ) ;
#7165=DIRECTION ( 'NONE',  ( -1.000000000000000000, 0.000000000000000000, 2.275957200481568888E-12 ) ) ;
#7187=ADVANCED_FACE ( 'NONE', ( #6305 ), #19041, .F. ) ;
#7218=CARTESIAN_POINT ( 'NONE',  ( 9.501873066115209099, 35.88348715183582982, -141.8183173552265828 ) ) ;
#7260=FACE_OUTER_BOUND ( 'NONE', #13525, .T. ) ;
#7282=CARTESIAN_POINT ( 'NONE',  ( 7.156080887020574544, 36.33197188641598530, -141.6458064976851290 ) ) ;
#7292=ORIENTED_EDGE ( 'NONE', *, *, #1006, .T. ) ;
#7333=CARTESIAN_POINT ( 'NONE',  ( 9.317029960348264694, 35.74200835522769637, -141.8948580844120784 ) ) ;
#7334=( GEOMETRIC_REPRESENTATION_CONTEXT ( 3 ) GLOBAL_UNCERTAINTY_ASSIGNED_CONTEXT ( ( #13755 ) ) GLOBAL_UNIT_ASSIGNED_CONTEXT ( ( #17237, #8534, #2737 ) ) REPRESENTATION_CONTEXT ( 'NONE', 'WORKASPACE' ) );
#7345=ORIENTED_EDGE ( 'NONE', *, *, #23519, .F. ) ;
#7361=ORIENTED_EDGE ( 'NONE', *, *, #14812, .T. ) ;
#7377=FACE_OUTER_BOUND ( 'NONE', #9581, .T. ) ;
#7414=DIRECTION ( 'NONE',  ( 1.000000000000000000, 0.000000000000000000, 0.000000000000000000 ) ) ;
#7457=EDGE_CURVE ( 'NONE', #6756, #19314, #19129, .T. ) ;
#7459=DIRECTION ( 'NONE',  ( 0.000000000000000000, 1.000000000000000000, 0.000000000000000000 ) ) ;
#7503=LINE ( 'NONE', #10948, #19996 ) ;
#7505=CARTESIAN_POINT ( 'NONE',  ( 7.661661249388155071, 35.75613975769173436, -141.8866982259418137 ) ) ;
#7520=EDGE_LOOP ( 'NONE', ( #9885, #6034 ) ) ;
#7552=CARTESIAN_POINT ( 'NONE',  ( 9.151339728411230112, 38.35153067472349875, -141.9520366269342446 ) ) ;
#7609=ORIENTED_EDGE ( 'NONE', *, *, #551, .T. ) ;
#7612=FACE_OUTER_BOUND ( 'NONE', #13376, .T. ) ;
#7622=CARTESIAN_POINT ( 'NONE',  ( 7.431199231726023591, 35.94753734600692496, -141.7876273308503414 ) ) ;
#7663=PLANE ( 'NONE',  #14201 ) ;
#7671=CARTESIAN_POINT ( 'NONE',  ( 9.744924853801363085, 37.83677071069875097, -141.6994869973544837 ) ) ;
#7697=VERTEX_POINT ( 'NONE', #19312 ) ;
#7708=CARTESIAN_POINT ( 'NONE',  ( -35.73252798949999942, 26.50000000000000000, -138.5552959529999839 ) ) ;
#7715=DIRECTION ( 'NONE',  ( 2.257171095940000041E-12, 1.003664318210000046E-28, 1.000000000000000000 ) ) ;
#7716=VERTEX_POINT ( 'NONE', #21348 ) ;
#7725=DIRECTION ( 'NONE',  ( -1.000000000000000000, 0.000000000000000000, 2.256683728769999802E-12 ) ) ;
#7735=DIRECTION ( 'NONE',  ( 1.000000000000000000, 2.602084704489999637E-17, -2.257171095940000041E-12 ) ) ;
#7737=CARTESIAN_POINT ( 'NONE',  ( 8.014315017057485946, 35.57994765775046631, -141.9976801201232490 ) ) ;
#7786=CARTESIAN_POINT ( 'NONE',  ( 9.337668468615847317, 38.24431173749859880, -141.8869580488046154 ) ) ;
#7815=LINE ( 'NONE', #22343, #14029 ) ;
#7821=ORIENTED_EDGE ( 'NONE', *, *, #6311, .F. ) ;
#7848=CARTESIAN_POINT ( 'NONE',  ( 7.657860202850368836, 35.75870734630790793, -141.8852171074365174 ) ) ;
#7855=LINE ( 'NONE', #3958, #11818 ) ;
#7875=CARTESIAN_POINT ( 'NONE',  ( -42.28007584270000052, 45.00000000000000000, -143.7573642109999810 ) ) ;
#7893=CARTESIAN_POINT ( 'NONE',  ( 8.845083429264123609, 38.45981370960942058, -142.0257885890056002 ) ) ;
#7894=CARTESIAN_POINT ( 'NONE',  ( 7.081342377746940642, 36.51003594057088009, -146.5072937552426708 ) ) ;
#7917=DIRECTION ( 'NONE',  ( 0.000000000000000000, 1.000000000000000000, 0.000000000000000000 ) ) ;
#7926=CARTESIAN_POINT ( 'NONE',  ( 8.500000000060001781, 38.50000000000000000, -146.0552959529999839 ) ) ;
#7936=SURFACE_STYLE_USAGE ( .BOTH. , #9832 ) ;
#7969=DIRECTION ( 'NONE',  ( 2.257171095940000041E-12, 1.003664318209372040E-28, 1.000000000000000000 ) ) ;
#8028=CARTESIAN_POINT ( 'NONE',  ( -30.50000000000000000, 37.00000000000000000, -149.0552959529999839 ) ) ;
#8032=ORIENTED_EDGE ( 'NONE', *, *, #17674, .F. ) ;
#8033=PLANE ( 'NONE',  #12916 ) ;
#8045=VECTOR ( 'NONE', #8889, 1000.000000000000000 ) ;
#8053=( NAMED_UNIT ( * ) PLANE_ANGLE_UNIT ( ) SI_UNIT ( $, .RADIAN. ) );
#8082=EDGE_CURVE ( 'NONE', #13979, #11330, #10568, .T. ) ;
#8120=VERTEX_POINT ( 'NONE', #21315 ) ;
#8150=LINE ( 'NONE', #18765, #20134 ) ;
#8158=CARTESIAN_POINT ( 'NONE',  ( 9.412777748462794136, 38.19458062236940776, -146.2522771197201905 ) ) ;
#8206=FACE_OUTER_BOUND ( 'NONE', #16893, .T. ) ;
#8216=ORIENTED_EDGE ( 'NONE', *, *, #22932, .F. ) ;
#8220=DIRECTION ( 'NONE',  ( 0.6689647316207368855, 1.740702895989316487E-17, -0.7432941462487078210 ) ) ;
#8255=ADVANCED_FACE ( 'NONE', ( #7260 ), #14527, .T. ) ;
#8279=CARTESIAN_POINT ( 'NONE',  ( 9.990149291296260614, 37.19975720979747535, -146.5492378968540095 ) ) ;
#8344=EDGE_CURVE ( 'NONE', #15836, #4200, #5587, .T. ) ;
#8353=EDGE_CURVE ( 'NONE', #19783, #22942, #20575, .T. ) ;
#8357=FACE_BOUND ( 'NONE', #5590, .T. ) ;
#8380=CARTESIAN_POINT ( 'NONE',  ( 7.099236174640187969, 36.46126239971106031, -146.4970002627034091 ) ) ;
#8390=CARTESIAN_POINT ( 'NONE',  ( -30.49999999990000177, 26.50000000000000000, -147.5552959529999839 ) ) ;
#8417=FILL_AREA_STYLE ('',( #10065 ) ) ;
#8466=ORIENTED_EDGE ( 'NONE', *, *, #19265, .T. ) ;
#8469=EDGE_CURVE ( 'NONE', #8753, #19783, #22475, .T. ) ;
#8471=CARTESIAN_POINT ( 'NONE',  ( 8.225765722546752201, 38.47477381467845703, -142.0366557234719096 ) ) ;
#8512=CARTESIAN_POINT ( 'NONE',  ( -30.49999999990000177, 29.00000000000000000, -140.5552959529999839 ) ) ;
#8534=( NAMED_UNIT ( * ) PLANE_ANGLE_UNIT ( ) SI_UNIT ( $, .RADIAN. ) );
#8552=CARTESIAN_POINT ( 'NONE',  ( -30.49999999990000177, 27.75000000000000000, -147.5552959529999839 ) ) ;
#8573=ORIENTED_EDGE ( 'NONE', *, *, #5987, .F. ) ;
#8577=CARTESIAN_POINT ( 'NONE',  ( 7.548835030704958093, 38.16033211785072154, -141.8404982651678097 ) ) ;
#8583=EDGE_CURVE ( 'NONE', #5898, #20128, #14117, .T. ) ;
#8590=CYLINDRICAL_SURFACE ( 'NONE', #21839, 2.000000000000001776 ) ;
#8624=CARTESIAN_POINT ( 'NONE',  ( 9.599503906027615940, 35.97803376242718798, -141.7732779960659570 ) ) ;
#8652=ORIENTED_EDGE ( 'NONE', *, *, #5752, .F. ) ;
#8687=ORIENTED_EDGE ( 'NONE', *, *, #6128, .F. ) ;
#8689=LINE ( 'NONE', #6803, #18211 ) ;
#8693=CARTESIAN_POINT ( 'NONE',  ( 7.752982640076552912, 38.30101337195760891, -141.9204103845874556 ) ) ;
#8749=CARTESIAN_POINT ( 'NONE',  ( 9.680021979716793012, 36.07364927583546432, -141.7332369982030116 ) ) ;
#8753=VERTEX_POINT ( 'NONE', #4081 ) ;
#8775=DIRECTION ( 'NONE',  ( 2.255140518769847203E-12, 0.000000000000000000, 1.000000000000000000 ) ) ;
#8779=VECTOR ( 'NONE', #1804, 1000.000000000000000 ) ;
#8793=LINE ( 'NONE', #10695, #20470 ) ;
#8813=CARTESIAN_POINT ( 'NONE',  ( -30.49999999990000177, 29.00000000000000000, -144.0552959529999839 ) ) ;
#8818=CARTESIAN_POINT ( 'NONE',  ( 7.279327523516623266, 36.12739586069235997, -141.7122832976002371 ) ) ;
#8829=CYLINDRICAL_SURFACE ( 'NONE', #22492, 2.500000000000002220 ) ;
#8857=EDGE_CURVE ( 'NONE', #16041, #23331, #526, .T. ) ;
#8869=CARTESIAN_POINT ( 'NONE',  ( 9.832297036978788540, 36.31037721551318498, -141.6522196278660033 ) ) ;
#8877=DIRECTION ( 'NONE',  ( 0.000000000000000000, 5.873289694040000105E-29, -1.000000000000000000 ) ) ;
#8889=DIRECTION ( 'NONE',  ( 0.000000000000000000, -1.000000000000000000, 0.000000000000000000 ) ) ;
#8893=FACE_OUTER_BOUND ( 'NONE', #21667, .T. ) ;
#8900=CARTESIAN_POINT ( 'NONE',  ( -46.50000000000000000, 47.50000000000000000, -148.4460207619999892 ) ) ;
#8910=VERTEX_POINT ( 'NONE', #5561 ) ;
#8917=ORIENTED_EDGE ( 'NONE', *, *, #1498, .T. ) ;
#8929=CARTESIAN_POINT ( 'NONE',  ( 7.628223423453324159, 38.22159669780096891, -141.8736084682009277 ) ) ;
#8981=CARTESIAN_POINT ( 'NONE',  ( 9.331285711378725978, 35.75141399242378526, -141.8894180609362650 ) ) ;
#9035=CARTESIAN_POINT ( 'NONE',  ( -37.89633983739999934, 26.50000000000000000, -139.8120018070000015 ) ) ;
#9042=CARTESIAN_POINT ( 'NONE',  ( 7.113920120768799649, 36.42649308455273882, -141.6219378633786050 ) ) ;
#9051=ORIENTED_EDGE ( 'NONE', *, *, #16286, .F. ) ;
#9089=EDGE_CURVE ( 'NONE', #22716, #6049, #4945, .T. ) ;
#9101=CARTESIAN_POINT ( 'NONE',  ( 9.039697480175762578, 35.60035037488847109, -141.9838786041871401 ) ) ;
#9108=ORIENTED_EDGE ( 'NONE', *, *, #17344, .T. ) ;
#9120=CIRCLE ( 'NONE', #1189, 2.500000000000002220 ) ;
#9140=VERTEX_POINT ( 'NONE', #20908 ) ;
#9150=DIRECTION ( 'NONE',  ( -1.000000000000000000, 1.734728570689999873E-18, 2.257171095940000041E-12 ) ) ;
#9201=ORIENTED_EDGE ( 'NONE', *, *, #4603, .F. ) ;
#9211=ADVANCED_FACE ( 'NONE', ( #19110 ), #8033, .T. ) ;
#9221=CARTESIAN_POINT ( 'NONE',  ( 8.598545881123929036, 38.50000000000002132, -142.0552959530002681 ) ) ;
#9251=CARTESIAN_POINT ( 'NONE',  ( 8.962923430288736171, 35.57285519170723376, -146.1079377423460244 ) ) ;
#9282=CARTESIAN_POINT ( 'NONE',  ( 8.120291913824591035, 35.54851131638615414, -142.0197959585554202 ) ) ;
#9306=EDGE_CURVE ( 'NONE', #11330, #6049, #19587, .T. ) ;
#9340=ORIENTED_EDGE ( 'NONE', *, *, #16151, .T. ) ;
#9348=CARTESIAN_POINT ( 'NONE',  ( -46.29070078880000239, 29.00000000000000000, -147.5552959540000018 ) ) ;
#9386=LINE ( 'NONE', #16661, #6384 ) ;
#9393=CARTESIAN_POINT ( 'NONE',  ( 8.188105526302459580, 35.53272852138334059, -142.0311810631520757 ) ) ;
#9420=DIRECTION ( 'NONE',  ( 0.000000000000000000, -1.000000000000000000, 0.000000000000000000 ) ) ;
#9441=CARTESIAN_POINT ( 'NONE',  ( 9.843919113198380089, 37.66802811340684798, -141.6458064975830951 ) ) ;
#9476=ADVANCED_FACE ( 'NONE', ( #15957 ), #21438, .F. ) ;
#9518=CARTESIAN_POINT ( 'NONE',  ( 7.661531047501870084, 35.75622639781018108, -141.8866492539494857 ) ) ;
#9544=VERTEX_POINT ( 'NONE', #11901 ) ;
#9568=CARTESIAN_POINT ( 'NONE',  ( 9.246789369175132833, 38.30178617907670002, -141.9207453424001528 ) ) ;
#9581=EDGE_LOOP ( 'NONE', ( #9625, #18870, #15666, #3940 ) ) ;
#9582=DIRECTION ( 'NONE',  ( 1.000000000000000000, 0.000000000000000000, 0.000000000000000000 ) ) ;
#9589=MECHANICAL_DESIGN_GEOMETRIC_PRESENTATION_REPRESENTATION('',(#20269),#5814);
#9597=DIRECTION ( 'NONE',  ( -0.7432941462487078210, 0.000000000000000000, -0.6689647316207368855 ) ) ;
#9625=ORIENTED_EDGE ( 'NONE', *, *, #9306, .F. ) ;
#9633=LINE ( 'NONE', #864, #227 ) ;
#9670=EDGE_LOOP ( 'NONE', ( #17205, #7345, #1722, #6331 ) ) ;
#9678=CARTESIAN_POINT ( 'NONE',  ( 9.342139795696894566, 38.24129265476425843, -141.8852171080566507 ) ) ;
#9680=CARTESIAN_POINT ( 'NONE',  ( 7.512097219667818848, 35.86684335154615155, -146.2851006690084148 ) ) ;
#9706=CARTESIAN_POINT ( 'NONE',  ( 9.252789717580752082, 38.29861131861105150, -146.1917200022118948 ) ) ;
#9770=DIRECTION ( 'NONE',  ( 1.000000000000000000, 0.000000000000000000, 0.000000000000000000 ) ) ;
#9791=CARTESIAN_POINT ( 'NONE',  ( 7.706401777573996803, 35.72582932411368262, -146.2064413145237154 ) ) ;
#9797=AXIS2_PLACEMENT_3D ( 'NONE', #20302, #3992, #22522 ) ;
#9815=CARTESIAN_POINT ( 'NONE',  ( -46.50000000000000000, 26.50000000000000000, -149.0552959529999839 ) ) ;
#9825=DIRECTION ( 'NONE',  ( -1.377713942929999840E-10, 1.000000000000000000, 0.000000000000000000 ) ) ;
#9832=SURFACE_SIDE_STYLE ('',( #15561 ) ) ;
#9869=DIRECTION ( 'NONE',  ( 0.000000000000000000, 1.000000000000000000, 0.000000000000000000 ) ) ;
#9885=ORIENTED_EDGE ( 'NONE', *, *, #14437, .F. ) ;
#9915=CARTESIAN_POINT ( 'NONE',  ( 8.301573612353688958, 35.50007106174292915, -146.0553492493495753 ) ) ;
#9922=CARTESIAN_POINT ( 'NONE',  ( -33.36626399469999882, 47.50000000000000000, -138.5552959529999839 ) ) ;
#9947=CARTESIAN_POINT ( 'NONE',  ( 9.105676901957313163, 38.37253232039734741, -146.1448649138488634 ) ) ;
#10001=DIRECTION ( 'NONE',  ( 2.602084747549999882E-17, -1.000000000000000000, -5.873289694040000105E-29 ) ) ;
#10032=CARTESIAN_POINT ( 'NONE',  ( 8.108968687586248336, 38.44920563369909416, -146.0924816361253704 ) ) ;
#10056=EDGE_CURVE ( 'NONE', #14263, #7697, #21805, .T. ) ;
#10060=VERTEX_POINT ( 'NONE', #14721 ) ;
#10063=CARTESIAN_POINT ( 'NONE',  ( -31.00000000000000000, 37.00000000000000000, -149.0552959529999839 ) ) ;
#10065=FILL_AREA_STYLE_COLOUR ( '', #21205 ) ;
#10086=LINE ( 'NONE', #12238, #22372 ) ;
#10094=CARTESIAN_POINT ( 'NONE',  ( -46.49999999989999822, 37.00000000000000000, -144.0552959529999839 ) ) ;
#10152=CARTESIAN_POINT ( 'NONE',  ( 7.009850708823739396, 36.80024279011028199, -146.5492378968398555 ) ) ;
#10168=VERTEX_POINT ( 'NONE', #8512 ) ;
#10182=CARTESIAN_POINT ( 'NONE',  ( 9.189953965651115553, 38.33228193160125130, -146.1707627155817590 ) ) ;
#10187=DIRECTION ( 'NONE',  ( -2.602084747549999882E-17, 1.000000000000000000, 5.873289694040000105E-29 ) ) ;
#10261=DIRECTION ( 'NONE',  ( 1.000000000000000000, 2.602084704489999637E-17, -2.257171095940000041E-12 ) ) ;
#10289=ORIENTED_EDGE ( 'NONE', *, *, #4515, .F. ) ;
#10381=ORIENTED_EDGE ( 'NONE', *, *, #5376, .T. ) ;
#10413=CARTESIAN_POINT ( 'NONE',  ( -30.49999999990000177, 29.00000000000000000, -140.5552959529999839 ) ) ;
#10459=EDGE_CURVE ( 'NONE', #10616, #5898, #304, .T. ) ;
#10469=VECTOR ( 'NONE', #10774, 1000.000000000000000 ) ;
#10477=CARTESIAN_POINT ( 'NONE',  ( 7.702812687520848911, 38.27075047946028974, -141.9023098454317449 ) ) ;
#10498=AXIS2_PLACEMENT_3D ( 'NONE', #4559, #22531, #9770 ) ;
#10526=CARTESIAN_POINT ( 'NONE',  ( 9.848540439720265383, 36.34242854357029984, -141.6431750412639303 ) ) ;
#10568=LINE ( 'NONE', #8552, #22795 ) ;
#10569=CARTESIAN_POINT ( 'NONE',  ( -30.49999999990000177, 37.00000000000000000, -144.0552959529999839 ) ) ;
#10595=CARTESIAN_POINT ( 'NONE',  ( 7.268891187599542114, 37.85696889435310197, -141.7067652898295478 ) ) ;
#10616=VERTEX_POINT ( 'NONE', #15399 ) ;
#10652=CARTESIAN_POINT ( 'NONE',  ( 9.731108812837232946, 36.14303110608750558, -141.7067652896560617 ) ) ;
#10660=PLANE ( 'NONE',  #4787 ) ;
#10695=CARTESIAN_POINT ( 'NONE',  ( -37.07045745269999770, 37.00000000000000000, -139.0687076600000012 ) ) ;
#10718=CARTESIAN_POINT ( 'NONE',  ( 7.774829774480637390, 38.31328358559468228, -141.9279471761695675 ) ) ;
#10728=CARTESIAN_POINT ( 'NONE',  ( -10.49999999989999822, 37.00000000000000000, -144.0552959529999839 ) ) ;
#10736=DIRECTION ( 'NONE',  ( -0.7432941462487078210, 0.000000000000000000, -0.6689647316207368855 ) ) ;
#10749=ORIENTED_EDGE ( 'NONE', *, *, #11680, .F. ) ;
#10773=PLANE ( 'NONE',  #6001 ) ;
#10774=DIRECTION ( 'NONE',  ( -1.000000000000000000, 0.000000000000000000, 2.256683728769999802E-12 ) ) ;
#10781=ORIENTED_EDGE ( 'NONE', *, *, #5376, .F. ) ;
#10787=EDGE_CURVE ( 'NONE', #19696, #11665, #20917, .T. ) ;
#10810=ADVANCED_FACE ( 'NONE', ( #19565 ), #15990, .F. ) ;
#10828=CARTESIAN_POINT ( 'NONE',  ( 7.009192481380154049, 36.80638614241070883, -141.5610522423419866 ) ) ;
#10867=CIRCLE ( 'NONE', #16584, 2.000000000000001776 ) ;
#10910=ORIENTED_EDGE ( 'NONE', *, *, #7457, .T. ) ;
#10928=ORIENTED_EDGE ( 'NONE', *, *, #12597, .T. ) ;
#10935=AXIS2_PLACEMENT_3D ( 'NONE', #16037, #17942, #5086 ) ;
#10948=CARTESIAN_POINT ( 'NONE',  ( -46.29070078859999882, 46.25000000000000000, -147.5552959529999839 ) ) ;
#10951=CARTESIAN_POINT ( 'NONE',  ( 7.848660272661017068, 35.64846932482826958, -141.9520366272613501 ) ) ;
#10963=FACE_BOUND ( 'NONE', #2431, .T. ) ;
#10993=AXIS2_PLACEMENT_3D ( 'NONE', #21793, #3813, #3691 ) ;
#11007=CARTESIAN_POINT ( 'NONE',  ( 9.101402224069296665, 38.37417018168379457, -141.9668508538656226 ) ) ;
#11009=VECTOR ( 'NONE', #10736, 1000.000000000000000 ) ;
#11039=CARTESIAN_POINT ( 'NONE',  ( 8.891031312599221081, 35.55079436630060741, -146.0924816361270189 ) ) ;
#11043=DIRECTION ( 'NONE',  ( 1.000000000000000000, 2.602084747549999882E-17, 0.000000000000000000 ) ) ;
#11076=VECTOR ( 'NONE', #7725, 1000.000000000000000 ) ;
#11082=FACE_OUTER_BOUND ( 'NONE', #12332, .T. ) ;
#11102=VERTEX_POINT ( 'NONE', #20673 ) ;
#11221=ORIENTED_EDGE ( 'NONE', *, *, #3206, .T. ) ;
#11226=ORIENTED_EDGE ( 'NONE', *, *, #8353, .F. ) ;
#11228=CARTESIAN_POINT ( 'NONE',  ( 9.961649902054594108, 37.34070208382173917, -141.5783375515752311 ) ) ;
#11235=VERTEX_POINT ( 'NONE', #16263 ) ;
#11275=CARTESIAN_POINT ( 'NONE',  ( -38.72222222220000276, 47.50000000000000000, -140.5552959529999839 ) ) ;
#11293=DIRECTION ( 'NONE',  ( 0.000000000000000000, 1.000000000000000000, 0.000000000000000000 ) ) ;
#11297=CARTESIAN_POINT ( 'NONE',  ( 7.406798920894477334, 35.97274762639648316, -141.7760678467019204 ) ) ;
#11320=ORIENTED_EDGE ( 'NONE', *, *, #5575, .T. ) ;
#11330=VERTEX_POINT ( 'NONE', #12181 ) ;
#11335=DIRECTION ( 'NONE',  ( 1.000000000000000000, 2.602084747549999882E-17, 0.000000000000000000 ) ) ;
#11344=CARTESIAN_POINT ( 'NONE',  ( 9.182696495386469593, 38.33585586787582855, -141.9420359944410279 ) ) ;
#11461=DIRECTION ( 'NONE',  ( -2.602084747549999882E-17, 1.000000000000000000, 5.873289694040000105E-29 ) ) ;
#11468=CARTESIAN_POINT ( 'NONE',  ( 9.374985222606666113, 38.21845128525978197, -141.8721224038111757 ) ) ;
#11495=CARTESIAN_POINT ( 'NONE',  ( 9.628134746819386081, 36.00655328089813167, -146.3507065506827303 ) ) ;
#11558=CARTESIAN_POINT ( 'NONE',  ( -30.49999999990000177, 45.00000000000000000, -140.5552959529999839 ) ) ;
#11580=CARTESIAN_POINT ( 'NONE',  ( 7.747210282536660664, 35.70138868135349242, -146.1917200021869689 ) ) ;
#11586=EDGE_LOOP ( 'NONE', ( #1702, #7082, #3127, #5653 ) ) ;
#11611=CARTESIAN_POINT ( 'NONE',  ( 9.918657622369268623, 37.48996405937540999, -146.5072937552601218 ) ) ;
#11665=VERTEX_POINT ( 'NONE', #3010 ) ;
#11680=EDGE_CURVE ( 'NONE', #8910, #20128, #6449, .T. ) ;
#11689=ORIENTED_EDGE ( 'NONE', *, *, #14197, .F. ) ;
#11699=CARTESIAN_POINT ( 'NONE',  ( 7.039467463307463646, 37.39727521495605345, -146.5309852632870786 ) ) ;
#11714=VERTEX_POINT ( 'NONE', #15617 ) ;
#11728=CARTESIAN_POINT ( 'NONE',  ( 9.795489902830604834, 36.24188551843280237, -146.4379907056267882 ) ) ;
#11768=CARTESIAN_POINT ( 'NONE',  ( -30.49999999990000177, 47.50000000000000000, -139.0552959529999839 ) ) ;
#11818=VECTOR ( 'NONE', #15012, 1000.000000000000000 ) ;
#11822=CARTESIAN_POINT ( 'NONE',  ( 7.894323098160722196, 35.62746767956905813, -146.1448649138240512 ) ) ;
#11883=PRODUCT_DEFINITION_SHAPE ( 'NONE', 'NONE',  #1074 ) ;
#11901=CARTESIAN_POINT ( 'NONE',  ( -46.29070078840000235, 47.50000000000000000, -147.5552959529999839 ) ) ;
#11933=ORIENTED_EDGE ( 'NONE', *, *, #11966, .F. ) ;
#11941=CARTESIAN_POINT ( 'NONE',  ( 8.107579704549820576, 35.53766814163076759, -146.0852624393625092 ) ) ;
#11952=LINE ( 'NONE', #8028, #4260 ) ;
#11966=EDGE_CURVE ( 'NONE', #14263, #21289, #7855, .T. ) ;
#11970=CARTESIAN_POINT ( 'NONE',  ( 9.770530770495106765, 36.20066385242879647, -146.4244424236570410 ) ) ;
#11971=AXIS2_PLACEMENT_3D ( 'NONE', #16097, #10261, #23119 ) ;
#12026=CARTESIAN_POINT ( 'NONE',  ( -46.00000000000000000, 26.50000000000000000, -149.5552959529999839 ) ) ;
#12134=VECTOR ( 'NONE', #20112, 1000.000000000000000 ) ;
#12141=EDGE_CURVE ( 'NONE', #4200, #19696, #1449, .T. ) ;
#12147=CARTESIAN_POINT ( 'NONE',  ( -46.00000000000000000, 47.50000000000000000, -149.0552959529999839 ) ) ;
#12181=CARTESIAN_POINT ( 'NONE',  ( -30.49999999990000177, 26.50000000000000000, -147.5552959529999839 ) ) ;
#12208=FACE_OUTER_BOUND ( 'NONE', #3316, .T. ) ;
#12238=CARTESIAN_POINT ( 'NONE',  ( -34.61111111099999960, 29.00000000000000000, -140.5552959529999839 ) ) ;
#12253=CARTESIAN_POINT ( 'NONE',  ( -46.00000000000000000, 47.50000000000000000, -149.5552959529999839 ) ) ;
#12275=CARTESIAN_POINT ( 'NONE',  ( 7.038350098255955700, 36.65929791540875016, -141.5783375516163005 ) ) ;
#12323=CARTESIAN_POINT ( 'NONE',  ( 9.797606456612053094, 36.24594602200216542, -141.6713346540966256 ) ) ;
#12332=EDGE_LOOP ( 'NONE', ( #1032, #19245, #5851, #15049 ) ) ;
#12333=CARTESIAN_POINT ( 'NONE',  ( 8.157178495121881312, 38.46135633873473836, -146.0837389892857061 ) ) ;
#12381=DIRECTION ( 'NONE',  ( -2.256988247090000272E-12, 0.000000000000000000, -1.000000000000000000 ) ) ;
#12386=CARTESIAN_POINT ( 'NONE',  ( 7.037218936158132543, 37.39203619355595976, -141.5783597022830236 ) ) ;
#12400=DIRECTION ( 'NONE',  ( 0.000000000000000000, 1.000000000000000000, 0.000000000000000000 ) ) ;
#12439=CARTESIAN_POINT ( 'NONE',  ( 9.120234899107126481, 35.63360340191769637, -141.9617131067784044 ) ) ;
#12465=AXIS2_PLACEMENT_3D ( 'NONE', #13464, #8220, #2886 ) ;
#12466=DIRECTION ( 'NONE',  ( -2.602084747549999882E-17, 1.000000000000000000, 5.873289694054760823E-29 ) ) ;
#12507=CARTESIAN_POINT ( 'NONE',  ( 7.498126930446614935, 38.11651284494442393, -141.8183173536806692 ) ) ;
#12554=CARTESIAN_POINT ( 'NONE',  ( -30.49999999990000177, 47.50000000000000000, -140.5552959529999839 ) ) ;
#12560=CARTESIAN_POINT ( 'NONE',  ( 8.891181416159669837, 35.55106431351824625, -142.0179551233528343 ) ) ;
#12565=EDGE_LOOP ( 'NONE', ( #17227, #22539, #11320, #7292 ) ) ;
#12567=ADVANCED_FACE ( 'NONE', ( #10963, #11082 ), #8829, .T. ) ;
#12597=EDGE_CURVE ( 'NONE', #11102, #10168, #21710, .T. ) ;
#12632=CARTESIAN_POINT ( 'NONE',  ( 7.668714288586619077, 38.24858600746667037, -141.8894180608807574 ) ) ;
#12681=CARTESIAN_POINT ( 'NONE',  ( 9.522541048056565316, 35.90250400897288330, -141.8090149961586803 ) ) ;
#12713=DIRECTION ( 'NONE',  ( -2.602084747549999882E-17, 1.000000000000000000, 5.873289694040000105E-29 ) ) ;
#12743=DIRECTION ( 'NONE',  ( 1.377713942929999840E-10, 1.000000000000000000, 0.000000000000000000 ) ) ;
#12745=CARTESIAN_POINT ( 'NONE',  ( 7.511313393277872841, 38.12817115245120192, -141.8241438720509962 ) ) ;
#12766=DIRECTION ( 'NONE',  ( 1.000000000000000000, 0.000000000000000000, 0.000000000000000000 ) ) ;
#12768=B_SPLINE_CURVE_WITH_KNOTS ( 'NONE', 3,
 ( #5574, #12825, #20098, #2137, #11039, #9251, #16521, #230, #22000, #5689, #20923, #4726, #6512, #11495, #6386, #11970, #11728, #13647, #20795, #17218, #4489, #13293, #8279, #4612, #2718, #11611, #932, #20562, #695, #18772, #2827, #16981, #8158, #6159, #9706, #10182, #19009, #2947, #9947, #15432, #15324, #7926 ),
 .UNSPECIFIED., .F., .F.,
 ( 4, 2, 2, 2, 2, 2, 2, 2, 2, 2, 2, 2, 2, 2, 2, 2, 2, 2, 2, 2, 4 ),
 ( 0.000000000000000000, 0.06249999999999189537, 0.09374999999998742672, 0.1093749999999862887, 0.1249999999999851508, 0.1874999999999937272, 0.2500000000000023315, 0.3125000000000108802, 0.3437500000000158762, 0.3750000000000208722, 0.5000000000000379696, 0.5625000000000442979, 0.5937500000000451861, 0.6250000000000461853, 0.6875000000000444089, 0.7500000000000426326, 0.8125000000000408562, 0.8437500000000387468, 0.8593750000000348610, 0.8750000000000309752, 1.000000000000000000 ),
 .UNSPECIFIED. ) ;
#12794=CARTESIAN_POINT ( 'NONE',  ( 9.336697666959173247, 35.75503528090352745, -141.8873347153283930 ) ) ;
#12825=CARTESIAN_POINT ( 'NONE',  ( 8.599236905806820985, 35.50003553908390330, -146.0553226073559756 ) ) ;
#12835=CARTESIAN_POINT ( 'NONE',  ( -30.49999999990000177, 46.25000000000000000, -140.5552959529999839 ) ) ;
#12854=CIRCLE ( 'NONE', #23500, 0.5000000000000004441 ) ;
#12890=EDGE_CURVE ( 'NONE', #11235, #896, #13196, .T. ) ;
#12898=VECTOR ( 'NONE', #190, 1000.000000000000000 ) ;
#12911=CARTESIAN_POINT ( 'NONE',  ( 9.790782907733147411, 37.76485605363462383, -141.6749984784336505 ) ) ;
#12916=AXIS2_PLACEMENT_3D ( 'NONE', #13509, #13872, #18995 ) ;
#12975=CARTESIAN_POINT ( 'NONE',  ( -31.00000000000000000, 26.50000000000000000, -149.0552959529999839 ) ) ;
#13012=CARTESIAN_POINT ( 'NONE',  ( -30.49999999990000177, 47.50000000000000000, -147.5552959529999839 ) ) ;
#13027=ORIENTED_EDGE ( 'NONE', *, *, #3588, .T. ) ;
#13040=ORIENTED_EDGE ( 'NONE', *, *, #8353, .T. ) ;
#13081=EDGE_LOOP ( 'NONE', ( #22121, #15912, #22669, #5233 ) ) ;
#13086=EDGE_LOOP ( 'NONE', ( #3256, #205, #16731, #2357, #2965, #16369 ) ) ;
#13095=CARTESIAN_POINT ( 'NONE',  ( 7.817303505803055330, 35.66414413158247498, -141.9420359948146881 ) ) ;
#13144=CARTESIAN_POINT ( 'NONE',  ( 9.447876141023428431, 38.16353938488455810, -141.8420144859424568 ) ) ;
#13167=CARTESIAN_POINT ( 'NONE',  ( -30.49999999990000177, 45.00000000000000000, -144.0552959529999839 ) ) ;
#13196=LINE ( 'NONE', #3937, #11076 ) ;
#13209=CARTESIAN_POINT ( 'NONE',  ( 8.085152496479286910, 35.55829573485724637, -142.0128484172198853 ) ) ;
#13238=CARTESIAN_POINT ( 'NONE',  ( -37.07045745269999770, 26.50000000000000000, -139.0687076600000012 ) ) ;
#13258=CARTESIAN_POINT ( 'NONE',  ( 9.339387736956417996, 38.24315306418434091, -141.8862908787521633 ) ) ;
#13293=CARTESIAN_POINT ( 'NONE',  ( 10.00000637188149177, 37.10042154059043185, -146.5552973561727583 ) ) ;
#13313=EDGE_CURVE ( 'NONE', #23177, #19038, #1901, .T. ) ;
#13326=VECTOR ( 'NONE', #755, 1000.000000000000000 ) ;
#13355=CIRCLE ( 'NONE', #6904, 2.500000000000002220 ) ;
#13376=EDGE_LOOP ( 'NONE', ( #4914, #8652, #16772, #11933, #18229 ) ) ;
#13383=CARTESIAN_POINT ( 'NONE',  ( 9.091636166211589654, 38.37840305069799030, -141.9696471534239777 ) ) ;
#13387=VERTEX_POINT ( 'NONE', #9348 ) ;
#13416=PRODUCT_DEFINITION_FORMATION_WITH_SPECIFIED_SOURCE ( 'ANY', '', #15507, .NOT_KNOWN. ) ;
#13432=EDGE_CURVE ( 'NONE', #16041, #15836, #5912, .T. ) ;
#13464=CARTESIAN_POINT ( 'NONE',  ( -36.49999999989999822, 37.00000000000000000, -138.5552959529999839 ) ) ;
#13472=CARTESIAN_POINT ( 'NONE',  ( -35.73252798949999942, 26.50000000000000000, -140.5552959529999839 ) ) ;
#13493=CARTESIAN_POINT ( 'NONE',  ( 7.746249104743133884, 38.30079617153757710, -146.1911047861169379 ) ) ;
#13509=CARTESIAN_POINT ( 'NONE',  ( -30.49999999990000177, 45.00000000000000000, -140.5552959529999839 ) ) ;
#13525=EDGE_LOOP ( 'NONE', ( #15657, #15004, #14911, #22358, #6849, #18177 ) ) ;
#13551=DIRECTION ( 'NONE',  ( 2.602084747549999882E-17, -1.000000000000000000, -5.873289694040000105E-29 ) ) ;
#13558=DIRECTION ( 'NONE',  ( 1.000000000000000000, 2.602084704489999637E-17, -2.257171095940000041E-12 ) ) ;
#13593=AXIS2_PLACEMENT_3D ( 'NONE', #10413, #16023, #19596 ) ;
#13647=CARTESIAN_POINT ( 'NONE',  ( 9.841496975946453674, 36.32698089522023821, -146.4634108040735896 ) ) ;
#13687=DIRECTION ( 'NONE',  ( -2.602084747549999882E-17, 1.000000000000000000, 5.873289694040000105E-29 ) ) ;
#13744=CARTESIAN_POINT ( 'NONE',  ( 7.000013276238538751, 37.20094785582138286, -146.5552931460549075 ) ) ;
#13755=UNCERTAINTY_MEASURE_WITH_UNIT (LENGTH_MEASURE( 1.000000000000000082E-05 ), #17237, 'distance_accuracy_value', 'NONE');
#13837=CARTESIAN_POINT ( 'NONE',  ( -35.73252798949999942, 37.00000000000000000, -138.5552959529999839 ) ) ;
#13872=DIRECTION ( 'NONE',  ( -2.602084747549999882E-17, 1.000000000000000000, 5.873289694040000105E-29 ) ) ;
#13874=VERTEX_POINT ( 'NONE', #12026 ) ;
#13889=LINE ( 'NONE', #17586, #19754 ) ;
#13979=VERTEX_POINT ( 'NONE', #14759 ) ;
#14008=ORIENTED_EDGE ( 'NONE', *, *, #22932, .T. ) ;
#14029=VECTOR ( 'NONE', #9825, 1000.000000000000000 ) ;
#14074=CARTESIAN_POINT ( 'NONE',  ( 7.400496094956046989, 38.02196623842161927, -141.7732779964421752 ) ) ;
#14115=CLOSED_SHELL ( 'NONE', ( #20077, #20617, #8255, #14407, #17138, #4429, #2695, #22624, #22034, #18697, #4718, #23195, #18064, #7187, #2482, #20281, #9211, #4254, #16520, #9476, #10810, #7148, #6989, #12567, #20051 ) ) ;
#14117=B_SPLINE_CURVE_WITH_KNOTS ( 'NONE', 3,
 ( #21405, #22952, #1305, #12333, #10032, #20890, #790, #17424, #20767, #4580, #13493, #21009, #15405, #17308, #1148, #17190, #2570, #4462, #908, #11699, #13744, #2919, #10152, #6486, #18975, #7894, #8380, #4700, #2689, #2457, #15652, #9680, #6359, #9791, #11580, #6244, #22911, #16955, #11822, #11941, #9915, #19096 ),
 .UNSPECIFIED., .F., .F.,
 ( 4, 2, 2, 2, 2, 2, 2, 2, 2, 2, 2, 2, 2, 2, 2, 2, 2, 2, 2, 2, 4 ),
 ( 0.000000000000000000, 0.06250000000000885403, 0.09375000000001450229, 0.1093750000000162370, 0.1250000000000179579, 0.1875000000000174860, 0.2500000000000169864, 0.3125000000000165423, 0.3437500000000161537, 0.3750000000000157652, 0.5000000000000107692, 0.5625000000000061062, 0.5937500000000037748, 0.6250000000000013323, 0.6874999999999966693, 0.7499999999999920064, 0.8124999999999873435, 0.8437499999999847899, 0.8593749999999865663, 0.8749999999999882316, 1.000000000000000000 ),
 .UNSPECIFIED. ) ;
#14125=CARTESIAN_POINT ( 'NONE',  ( 9.736748385090495006, 36.15119022970048235, -141.7037997430031169 ) ) ;
#14140=ORIENTED_EDGE ( 'NONE', *, *, #6311, .T. ) ;
#14158=PLANE ( 'NONE',  #17744 ) ;
#14190=CARTESIAN_POINT ( 'NONE',  ( 7.243343564704193049, 36.18094154607518220, -141.6932697408899173 ) ) ;
#14193=FACE_OUTER_BOUND ( 'NONE', #19729, .T. ) ;
#14197=EDGE_CURVE ( 'NONE', #10168, #21289, #10086, .T. ) ;
#14201=AXIS2_PLACEMENT_3D ( 'NONE', #4223, #11461, #11335 ) ;
#14206=CARTESIAN_POINT ( 'NONE',  ( -44.50000000000000000, 37.00000000000000000, -148.4460207619999892 ) ) ;
#14223=CARTESIAN_POINT ( 'NONE',  ( -30.49999999990000177, 47.50000000000000000, -148.3052959529999839 ) ) ;
#14234=ORIENTED_EDGE ( 'NONE', *, *, #12141, .T. ) ;
#14243=CARTESIAN_POINT ( 'NONE',  ( 9.962781063757809363, 36.60796380593278343, -141.5783597023373943 ) ) ;
#14251=DIRECTION ( 'NONE',  ( 1.000000000000000000, 0.000000000000000000, -2.257171095940000041E-12 ) ) ;
#14252=LINE ( 'NONE', #16038, #10469 ) ;
#14263=VERTEX_POINT ( 'NONE', #17718 ) ;
#14303=CARTESIAN_POINT ( 'NONE',  ( 7.930184371052885872, 38.38757070224898627, -141.9757830863086667 ) ) ;
#14344=AXIS2_PLACEMENT_3D ( 'NONE', #21340, #21696, #5033 ) ;
#14358=CARTESIAN_POINT ( 'NONE',  ( 9.247017358121205177, 35.69898662692506264, -141.9204103852138417 ) ) ;
#14360=CARTESIAN_POINT ( 'NONE',  ( -33.36626399469999882, 26.50000000000000000, -138.5552959529999839 ) ) ;
#14407=ADVANCED_FACE ( 'NONE', ( #8893 ), #23311, .T. ) ;
#14425=FACE_OUTER_BOUND ( 'NONE', #21779, .T. ) ;
#14426=CARTESIAN_POINT ( 'NONE',  ( 7.456043044519751639, 38.07711648188232800, -141.7992203782033300 ) ) ;
#14437=EDGE_CURVE ( 'NONE', #11235, #18574, #23138, .T. ) ;
#14482=CARTESIAN_POINT ( 'NONE',  ( 9.451164963400199071, 35.83966787717029234, -141.8404982676872237 ) ) ;
#14527=PLANE ( 'NONE',  #10993 ) ;
#14551=CARTESIAN_POINT ( 'NONE',  ( 7.000004459280741109, 37.19153793952586540, -141.5553035005532649 ) ) ;
#14595=CARTESIAN_POINT ( 'NONE',  ( 8.774234277345202671, 35.52522618527662956, -142.0366557234719380 ) ) ;
#14663=CYLINDRICAL_SURFACE ( 'NONE', #18315, 0.5000000000000004441 ) ;
#14721=CARTESIAN_POINT ( 'NONE',  ( -35.73252798949999942, 47.50000000000000000, -138.5552959529999839 ) ) ;
#14728=ORIENTED_EDGE ( 'NONE', *, *, #4417, .F. ) ;
#14740=ORIENTED_EDGE ( 'NONE', *, *, #3588, .F. ) ;
#14759=CARTESIAN_POINT ( 'NONE',  ( -30.49999999990000177, 29.00000000000000000, -147.5552959529999839 ) ) ;
#14812=EDGE_CURVE ( 'NONE', #4078, #11102, #16414, .T. ) ;
#14817=VECTOR ( 'NONE', #4382, 1000.000000000000000 ) ;
#14892=CARTESIAN_POINT ( 'NONE',  ( 7.437582298410791992, 35.94108727011604287, -141.7906281409924816 ) ) ;
#14898=VECTOR ( 'NONE', #2423, 1000.000000000000000 ) ;
#14911=ORIENTED_EDGE ( 'NONE', *, *, #5987, .T. ) ;
#14913=EDGE_CURVE ( 'NONE', #20128, #5898, #12768, .T. ) ;
#14941=CARTESIAN_POINT ( 'NONE',  ( 9.562417701932698577, 38.05891272967145511, -141.7906281408962172 ) ) ;
#14942=EDGE_CURVE ( 'NONE', #21515, #4078, #22390, .T. ) ;
#14964=EDGE_CURVE ( 'NONE', #6049, #13387, #7815, .T. ) ;
#15003=CARTESIAN_POINT ( 'NONE',  ( 7.304793568844493379, 36.09237029978162070, -141.7255920985726902 ) ) ;
#15004=ORIENTED_EDGE ( 'NONE', *, *, #6723, .F. ) ;
#15012=DIRECTION ( 'NONE',  ( 0.7432941462487078210, 0.000000000000000000, 0.6689647316207368855 ) ) ;
#15049=ORIENTED_EDGE ( 'NONE', *, *, #1973, .T. ) ;
#15051=CARTESIAN_POINT ( 'NONE',  ( 9.568800768469639451, 38.05246265392671745, -141.7876273308280872 ) ) ;
#15118=CARTESIAN_POINT ( 'NONE',  ( 7.500784825167067460, 35.87811771440581765, -141.8201969968949925 ) ) ;
#15141=AXIS2_PLACEMENT_3D ( 'NONE', #607, #13551, #15238 ) ;
#15149=DIRECTION ( 'NONE',  ( 0.7432941462487078210, 0.000000000000000000, 0.6689647316207368855 ) ) ;
#15172=CARTESIAN_POINT ( 'NONE',  ( 9.720672476820208630, 37.87260413900303746, -141.7122832975126414 ) ) ;
#15219=( LENGTH_UNIT ( ) NAMED_UNIT ( * ) SI_UNIT ( .MILLI., .METRE. ) );
#15238=DIRECTION ( 'NONE',  ( 0.000000000000000000, 5.873289694040000105E-29, -1.000000000000000000 ) ) ;
#15251=CARTESIAN_POINT ( 'NONE',  ( -30.49999999990000177, 26.50000000000000000, -148.3052959529999839 ) ) ;
#15324=CARTESIAN_POINT ( 'NONE',  ( 8.698426387723953823, 38.49992893826069462, -146.0553492493478132 ) ) ;
#15385=CARTESIAN_POINT ( 'NONE',  ( -30.99999999989999822, 26.50000000000000000, -138.5552959529999839 ) ) ;
#15399=CARTESIAN_POINT ( 'NONE',  ( 8.500000000060001781, 38.50000000000000000, -142.0552959529999839 ) ) ;
#15405=CARTESIAN_POINT ( 'NONE',  ( 7.510813698219587664, 38.13186516299664675, -146.2857056571632199 ) ) ;
#15432=CARTESIAN_POINT ( 'NONE',  ( 8.892420295525585772, 38.46233185836359780, -146.0852624393696146 ) ) ;
#15490=EDGE_CURVE ( 'NONE', #11102, #8120, #16120, .T. ) ;
#15507=PRODUCT ( 'Latch Bolt Assembly', 'Latch Bolt Assembly', '', ( #2019 ) ) ;
#15561=SURFACE_STYLE_FILL_AREA ( #8417 ) ;
#15580=ORIENTED_EDGE ( 'NONE', *, *, #11966, .T. ) ;
#15593=VECTOR ( 'NONE', #5175, 1000.000000000000000 ) ;
#15617=CARTESIAN_POINT ( 'NONE',  ( -37.07045745269999770, 47.50000000000000000, -139.0687076600000012 ) ) ;
#15652=CARTESIAN_POINT ( 'NONE',  ( 7.370503126277467842, 36.00792309428232585, -146.3513483205678369 ) ) ;
#15657=ORIENTED_EDGE ( 'NONE', *, *, #6232, .T. ) ;
#15666=ORIENTED_EDGE ( 'NONE', *, *, #18272, .T. ) ;
#15717=CYLINDRICAL_SURFACE ( 'NONE', #719, 2.000000000000007994 ) ;
#15730=DIRECTION ( 'NONE',  ( 1.000000000000000000, 0.000000000000000000, 0.000000000000000000 ) ) ;
#15738=CARTESIAN_POINT ( 'NONE',  ( 8.155284681625030174, 38.46058812810072425, -142.0263608015445982 ) ) ;
#15797=DIRECTION ( 'NONE',  ( 2.257171095940000041E-12, 1.003664318210000046E-28, 1.000000000000000000 ) ) ;
#15807=FILL_AREA_STYLE ('',( #6642 ) ) ;
#15836=VERTEX_POINT ( 'NONE', #11558 ) ;
#15849=CARTESIAN_POINT ( 'NONE',  ( 7.190767566730844607, 36.26753466208879928, -141.6649243765320421 ) ) ;
#15899=CARTESIAN_POINT ( 'NONE',  ( 9.077094367341661751, 35.61544623144256150, -141.9737733526287116 ) ) ;
#15900=AXIS2_PLACEMENT_3D ( 'NONE', #21966, #10001, #22633 ) ;
#15912=ORIENTED_EDGE ( 'NONE', *, *, #15989, .F. ) ;
#15938=FACE_OUTER_BOUND ( 'NONE', #4615, .T. ) ;
#15939=AXIS2_PLACEMENT_3D ( 'NONE', #2080, #5517, #12766 ) ;
#15957=FACE_OUTER_BOUND ( 'NONE', #7520, .T. ) ;
#15974=CARTESIAN_POINT ( 'NONE',  ( 7.443892100749126328, 38.06519908407426556, -141.7935801463240182 ) ) ;
#15989=EDGE_CURVE ( 'NONE', #21976, #10060, #17521, .T. ) ;
#15990=CYLINDRICAL_SURFACE ( 'NONE', #3811, 1.500000000000001332 ) ;
#16005=EDGE_LOOP ( 'NONE', ( #17916, #8687, #9108, #14740 ) ) ;
#16023=DIRECTION ( 'NONE',  ( -2.257171095940000041E-12, -1.003664318210000046E-28, -1.000000000000000000 ) ) ;
#16028=CARTESIAN_POINT ( 'NONE',  ( 9.872691270914929262, 36.39514331228942012, -141.6295540220486089 ) ) ;
#16037=CARTESIAN_POINT ( 'NONE',  ( -33.00000000000000000, 37.00000000000000000, -149.5552959529999839 ) ) ;
#16038=CARTESIAN_POINT ( 'NONE',  ( -38.50000000000000000, 26.50000000000000000, -149.5552959529999839 ) ) ;
#16041=VERTEX_POINT ( 'NONE', #6804 ) ;
#16073=DIRECTION ( 'NONE',  ( 0.000000000000000000, 1.000000000000000000, 0.000000000000000000 ) ) ;
#16085=DIRECTION ( 'NONE',  ( -2.602084747549999882E-17, 1.000000000000000000, 5.873289694040000105E-29 ) ) ;
#16094=CARTESIAN_POINT ( 'NONE',  ( 7.319978021535112234, 37.92635072559305343, -141.7332369987670404 ) ) ;
#16097=CARTESIAN_POINT ( 'NONE',  ( -30.49999999990000177, 37.00000000000000000, -144.0552959529999839 ) ) ;
#16120=LINE ( 'NONE', #19685, #21122 ) ;
#16144=ORIENTED_EDGE ( 'NONE', *, *, #6128, .T. ) ;
#16147=CARTESIAN_POINT ( 'NONE',  ( 10.00000222906343339, 37.09571658197103261, -141.5552923336952915 ) ) ;
#16151=EDGE_CURVE ( 'NONE', #23331, #9544, #7503, .T. ) ;
#16159=ORIENTED_EDGE ( 'NONE', *, *, #10787, .T. ) ;
#16173=DIRECTION ( 'NONE',  ( -1.000000000000000000, 1.734728570689999873E-18, 2.257171095940000041E-12 ) ) ;
#16190=VECTOR ( 'NONE', #1684, 1000.000000000000000 ) ;
#16212=CARTESIAN_POINT ( 'NONE',  ( 7.477458949725431125, 38.09749598883478683, -141.8090149951282797 ) ) ;
#16217=FACE_OUTER_BOUND ( 'NONE', #12565, .T. ) ;
#16263=CARTESIAN_POINT ( 'NONE',  ( 14.50000000010000001, 39.50000000000000000, -144.0552959529999839 ) ) ;
#16265=CARTESIAN_POINT ( 'NONE',  ( 8.787969351399857132, 35.52785605379246903, -142.0347430632536714 ) ) ;
#16286=EDGE_CURVE ( 'NONE', #896, #9140, #18055, .T. ) ;
#16291=CARTESIAN_POINT ( 'NONE',  ( -30.99999999989999822, 37.00000000000000000, -139.0552959529999839 ) ) ;
#16298=CARTESIAN_POINT ( 'NONE',  ( -30.49999999990000177, 29.00000000000000000, -140.5552959529999839 ) ) ;
#16331=CARTESIAN_POINT ( 'NONE',  ( 7.135907599097732756, 36.37446523411252741, -141.6344350119672981 ) ) ;
#16348=DIRECTION ( 'NONE',  ( 2.602084747549999882E-17, -1.000000000000000000, -5.873289694040000105E-29 ) ) ;
#16369=ORIENTED_EDGE ( 'NONE', *, *, #10787, .F. ) ;
#16384=CARTESIAN_POINT ( 'NONE',  ( 9.057761017886996058, 35.60753996401869159, -141.9790531660381703 ) ) ;
#16403=ORIENTED_EDGE ( 'NONE', *, *, #21347, .F. ) ;
#16414=LINE ( 'NONE', #2376, #1141 ) ;
#16489=CARTESIAN_POINT ( 'NONE',  ( 8.500000000060001781, 38.50000000000000000, -142.0552959529999839 ) ) ;
#16508=VERTEX_POINT ( 'NONE', #8900 ) ;
#16520=ADVANCED_FACE ( 'NONE', ( #5471 ), #1791, .T. ) ;
#16521=CARTESIAN_POINT ( 'NONE',  ( 8.986817037251329410, 35.58084844828771764, -146.1134792699400009 ) ) ;
#16584=AXIS2_PLACEMENT_3D ( 'NONE', #17901, #283, #7414 ) ;
#16632=ORIENTED_EDGE ( 'NONE', *, *, #10056, .T. ) ;
#16661=CARTESIAN_POINT ( 'NONE',  ( -38.72222222220000276, 27.75000000000000000, -140.5552959529999839 ) ) ;
#16669=CARTESIAN_POINT ( 'NONE',  ( 7.609232054053188143, 35.79289365172241588, -141.8657226768378052 ) ) ;
#16702=VECTOR ( 'NONE', #7459, 1000.000000000000000 ) ;
#16719=CARTESIAN_POINT ( 'NONE',  ( 9.633444787484091165, 37.98285379039364074, -141.7565619020742531 ) ) ;
#16731=ORIENTED_EDGE ( 'NONE', *, *, #1498, .F. ) ;
#16772=ORIENTED_EDGE ( 'NONE', *, *, #14197, .T. ) ;
#16786=LINE ( 'NONE', #2058, #18860 ) ;
#16791=CARTESIAN_POINT ( 'NONE',  ( 7.883839590577690792, 35.63231902296612930, -141.9625758180283128 ) ) ;
#16827=COLOUR_RGB ( '', 0.08235294, 0.09019608, 0.10196078) ;
#16841=CARTESIAN_POINT ( 'NONE',  ( 9.390767940384391110, 38.20710635247810671, -141.8657226791105188 ) ) ;
#16893=EDGE_LOOP ( 'NONE', ( #21162, #5177, #20311, #22323 ) ) ;
#16899=ORIENTED_EDGE ( 'NONE', *, *, #4295, .F. ) ;
#16903=CARTESIAN_POINT ( 'NONE',  ( 7.708627906697441468, 35.72455532609014028, -141.9048323918832750 ) ) ;
#16911=AXIS2_PLACEMENT_3D ( 'NONE', #6195, #7735, #380 ) ;
#16931=LINE ( 'NONE', #7875, #3303 ) ;
#16954=CARTESIAN_POINT ( 'NONE',  ( 9.338468952632505093, 38.24377360218669963, -141.8866492539555111 ) ) ;
#16955=CARTESIAN_POINT ( 'NONE',  ( 7.874234281797447110, 35.63651660423768419, -146.1507818849889873 ) ) ;
#16981=CARTESIAN_POINT ( 'NONE',  ( 9.487902780448600026, 38.13315664843509012, -146.2851006690217162 ) ) ;
#17045=DIRECTION ( 'NONE',  ( -2.602084747549999882E-17, 1.000000000000000000, 5.873289694040000105E-29 ) ) ;
#17084=DIRECTION ( 'NONE',  ( 0.000000000000000000, 0.000000000000000000, 1.000000000000000000 ) ) ;
#17129=ORIENTED_EDGE ( 'NONE', *, *, #5575, .F. ) ;
#17138=ADVANCED_FACE ( 'NONE', ( #8357, #14193 ), #3024, .T. ) ;
#17190=CARTESIAN_POINT ( 'NONE',  ( 7.229469229562214494, 37.79933614746168757, -146.4244424236882480 ) ) ;
#17196=ORIENTED_EDGE ( 'NONE', *, *, #17344, .F. ) ;
#17205=ORIENTED_EDGE ( 'NONE', *, *, #4295, .T. ) ;
#17218=CARTESIAN_POINT ( 'NONE',  ( 9.960532536797563452, 36.60272478500484539, -146.5309852632849470 ) ) ;
#17227=ORIENTED_EDGE ( 'NONE', *, *, #4515, .T. ) ;
#17237=( LENGTH_UNIT ( ) NAMED_UNIT ( * ) SI_UNIT ( .MILLI., .METRE. ) );
#17245=CARTESIAN_POINT ( 'NONE',  ( -46.50000000000000000, 47.50000000000000000, -148.7506583580000097 ) ) ;
#17259=CARTESIAN_POINT ( 'NONE',  ( -44.50000000000000000, 29.00000000000000000, -148.4460207619999892 ) ) ;
#17308=CARTESIAN_POINT ( 'NONE',  ( 7.371865253256605577, 37.99344671901626214, -146.3507065507166658 ) ) ;
#17311=CARTESIAN_POINT ( 'NONE',  ( -38.72222222220000276, 45.00000000000000000, -140.5552959529999839 ) ) ;
#17344=EDGE_CURVE ( 'NONE', #22716, #16508, #9633, .T. ) ;
#17370=DIRECTION ( 'NONE',  ( -2.257171095940000041E-12, 0.000000000000000000, -1.000000000000000000 ) ) ;
#17401=DIRECTION ( 'NONE',  ( 0.000000000000000000, 1.000000000000000000, 0.000000000000000000 ) ) ;
#17403=CARTESIAN_POINT ( 'NONE',  ( 8.500000000060001781, 38.50000000000000000, -142.0552959529999839 ) ) ;
#17419=( GEOMETRIC_REPRESENTATION_CONTEXT ( 3 ) GLOBAL_UNCERTAINTY_ASSIGNED_CONTEXT ( ( #21847 ) ) GLOBAL_UNIT_ASSIGNED_CONTEXT ( ( #15219, #8053, #20804 ) ) REPRESENTATION_CONTEXT ( 'NONE', 'WORKASPACE' ) );
#17424=CARTESIAN_POINT ( 'NONE',  ( 7.965536613495201479, 38.40185705422590701, -146.1252975212037484 ) ) ;
#17433=FACE_OUTER_BOUND ( 'NONE', #20809, .T. ) ;
#17454=CARTESIAN_POINT ( 'NONE',  ( -30.99999999989999822, 26.50000000000000000, -139.0552959529999839 ) ) ;
#17521=LINE ( 'NONE', #13837, #1013 ) ;
#17563=VECTOR ( 'NONE', #3548, 1000.000000000000000 ) ;
#17586=CARTESIAN_POINT ( 'NONE',  ( -46.50000000000000000, 26.50000000000000000, -148.7506583580000097 ) ) ;
#17595=ORIENTED_EDGE ( 'NONE', *, *, #20846, .T. ) ;
#17599=ORIENTED_EDGE ( 'NONE', *, *, #8583, .T. ) ;
#17643=CARTESIAN_POINT ( 'NONE',  ( 7.202393543502077833, 37.75405397796894391, -141.6713346540711314 ) ) ;
#17674=EDGE_CURVE ( 'NONE', #4200, #23177, #17972, .T. ) ;
#17691=CARTESIAN_POINT ( 'NONE',  ( 8.500000000060001781, 35.50000000000000000, -142.0552959529999839 ) ) ;
#17695=LINE ( 'NONE', #17812, #22787 ) ;
#17700=CARTESIAN_POINT ( 'NONE',  ( 8.500000000060001781, 35.50000000000000000, -146.0552959529999839 ) ) ;
#17711=ORIENTED_EDGE ( 'NONE', *, *, #4730, .F. ) ;
#17718=CARTESIAN_POINT ( 'NONE',  ( -45.83792946319999828, 29.00000000000000000, -146.9594324700000243 ) ) ;
#17730=DIRECTION ( 'NONE',  ( 0.000000000000000000, -1.000000000000000000, 0.000000000000000000 ) ) ;
#17731=DIRECTION ( 'NONE',  ( 0.000000000000000000, 1.000000000000000000, 0.000000000000000000 ) ) ;
#17741=CIRCLE ( 'NONE', #10498, 2.000000000000001776 ) ;
#17744=AXIS2_PLACEMENT_3D ( 'NONE', #16298, #1790, #1678 ) ;
#17753=CARTESIAN_POINT ( 'NONE',  ( 7.050624870945322087, 36.61023527371315822, -141.5855402290984557 ) ) ;
#17765=EDGE_LOOP ( 'NONE', ( #1472, #5221, #11226, #23472 ) ) ;
#17791=VECTOR ( 'NONE', #798, 1000.000000000000000 ) ;
#17805=CARTESIAN_POINT ( 'NONE',  ( 9.551261401524259398, 35.93001144567825378, -141.7958383017457038 ) ) ;
#17812=CARTESIAN_POINT ( 'NONE',  ( -38.39535039420000118, 47.50000000000000000, -147.5552959529999839 ) ) ;
#17814=VECTOR ( 'NONE', #21721, 1000.000000000000000 ) ;
#17872=AXIS2_PLACEMENT_3D ( 'NONE', #7059, #16348, #53 ) ;
#17881=CARTESIAN_POINT ( 'NONE',  ( 7.127308729211550009, 37.60485668770037648, -141.6295540220406508 ) ) ;
#17901=CARTESIAN_POINT ( 'NONE',  ( -35.73252798949999942, 47.50000000000000000, -140.5552959529999839 ) ) ;
#17916=ORIENTED_EDGE ( 'NONE', *, *, #1006, .F. ) ;
#17942=DIRECTION ( 'NONE',  ( 2.257171095940000041E-12, 1.003664318210000046E-28, 1.000000000000000000 ) ) ;
#17972=LINE ( 'NONE', #18086, #16190 ) ;
#17999=CARTESIAN_POINT ( 'NONE',  ( 7.663302333319010451, 38.24496471919625407, -141.8873347153860607 ) ) ;
#18009=EDGE_CURVE ( 'NONE', #8753, #13874, #14252, .T. ) ;
#18040=VECTOR ( 'NONE', #4779, 1000.000000000000000 ) ;
#18052=ORIENTED_EDGE ( 'NONE', *, *, #12597, .F. ) ;
#18055=CIRCLE ( 'NONE', #16911, 2.500000000000002220 ) ;
#18064=ADVANCED_FACE ( 'NONE', ( #23296 ), #10660, .T. ) ;
#18073=DIRECTION ( 'NONE',  ( 0.000000000000000000, -1.000000000000000000, 0.000000000000000000 ) ) ;
#18086=CARTESIAN_POINT ( 'NONE',  ( -34.61111111099999960, 47.50000000000000000, -140.5552959529999839 ) ) ;
#18113=CARTESIAN_POINT ( 'NONE',  ( 7.085192309373985253, 36.50051581081366692, -141.6055286362093000 ) ) ;
#18164=CARTESIAN_POINT ( 'NONE',  ( 8.598996733729995512, 35.50242794714858263, -142.0534435078296269 ) ) ;
#18177=ORIENTED_EDGE ( 'NONE', *, *, #14942, .F. ) ;
#18183=CARTESIAN_POINT ( 'NONE',  ( -45.83792946319999828, 37.00000000000000000, -146.9594324700000243 ) ) ;
#18203=ORIENTED_EDGE ( 'NONE', *, *, #7457, .F. ) ;
#18211=VECTOR ( 'NONE', #23111, 1000.000000000000000 ) ;
#18229=ORIENTED_EDGE ( 'NONE', *, *, #21701, .F. ) ;
#18236=CARTESIAN_POINT ( 'NONE',  ( 8.177875869394885200, 35.53494891409558676, -142.0295714736785442 ) ) ;
#18246=DIRECTION ( 'NONE',  ( 0.000000000000000000, -1.000000000000000000, 0.000000000000000000 ) ) ;
#18247=LINE ( 'NONE', #2308, #19069 ) ;
#18252=AXIS2_PLACEMENT_3D ( 'NONE', #18302, #2017, #9582 ) ;
#18260=CARTESIAN_POINT ( 'NONE',  ( -38.39535039439999764, 29.00000000000000000, -147.5552959529999839 ) ) ;
#18272=EDGE_CURVE ( 'NONE', #13979, #13387, #1967, .T. ) ;
#18288=EDGE_CURVE ( 'NONE', #10060, #11714, #10867, .T. ) ;
#18290=CARTESIAN_POINT ( 'NONE',  ( 8.699041270020327232, 38.49025597642661722, -142.0478759868930183 ) ) ;
#18302=CARTESIAN_POINT ( 'NONE',  ( -44.50000000000000000, 26.50000000000000000, -148.4460207619999892 ) ) ;
#18315=AXIS2_PLACEMENT_3D ( 'NONE', #21580, #23470, #7165 ) ;
#18324=ORIENTED_EDGE ( 'NONE', *, *, #23496, .T. ) ;
#18380=ORIENTED_EDGE ( 'NONE', *, *, #10459, .T. ) ;
#18395=CARTESIAN_POINT ( 'NONE',  ( 9.914807690894544834, 37.49948418880605772, -141.6055286361879553 ) ) ;
#18457=CARTESIAN_POINT ( 'NONE',  ( 7.350211351706771090, 36.03637995787053683, -141.7484567678159806 ) ) ;
#18484=EDGE_CURVE ( 'NONE', #13874, #22942, #16786, .T. ) ;
#18502=CARTESIAN_POINT ( 'NONE',  ( 9.864092401084887385, 37.62553476576535161, -141.6344350118990576 ) ) ;
#18509=VECTOR ( 'NONE', #5417, 1000.000000000000000 ) ;
#18510=ORIENTED_EDGE ( 'NONE', *, *, #16151, .F. ) ;
#18573=CARTESIAN_POINT ( 'NONE',  ( 7.625014772252407091, 35.78154871851074148, -141.8721224017280917 ) ) ;
#18574=VERTEX_POINT ( 'NONE', #22722 ) ;
#18629=CARTESIAN_POINT ( 'NONE',  ( 9.033660455730478489, 38.40283821535013686, -141.9858703027461786 ) ) ;
#18658=B_SPLINE_CURVE_WITH_KNOTS ( 'NONE', 3,
 ( #17403, #1124, #22892, #6575, #21104, #19308, #8471, #22998, #15738, #6688, #21574, #23464, #7040, #3480, #14303, #21815, #1823, #23351, #10718, #8693, #1709, #10477, #21697, #21341, #12632, #3242, #17999, #5499, #8929, #6807, #8577, #12745, #12507, #16212, #1597, #14426, #19903, #15974, #14074, #3713, #16094, #3356, #23116, #5383, #10595, #38, #20018, #3602, #17643, #5256, #19788, #5034, #17881, #7160, #12386, #14551, #6929, #10828, #12275, #17753, #1351, #18113, #19549, #19661, #9042, #16331, #7282, #15849, #1471, #23234, #14190, #21455, #5135, #8818, #15003, #18457, #20602, #614, #11297, #20366, #7622, #4062, #14892, #15118, #18701, #16669, #18573, #2061, #2297, #7848, #383, #7505, #5839, #9518, #16903, #22153, #13095, #10951, #16791, #2412, #5725, #504, #2172, #7737, #13209, #9282, #153, #18236, #9393, #22264, #22040, #5954 ),
 .UNSPECIFIED., .F., .F.,
 ( 4, 2, 1, 2, 2, 2, 1, 1, 2, 2, 2, 2, 1, 1, 1, 2, 2, 2, 2, 2, 1, 2, 2, 2, 2, 1, 2, 2, 2, 1, 2, 2, 2, 2, 2, 1, 2, 2, 2, 1, 1, 2, 2, 2, 2, 1, 1, 2, 2, 2, 2, 1, 1, 1, 2, 2, 2, 1, 1, 2, 2, 2, 1, 2, 2, 4 ),
 ( 0.000000000000000000, 0.03124999999964979402, 0.04687499999947458001, 0.05468749999938697648, 0.06249999999929936600, 0.09374999999895526626, 0.1093749999987843197, 0.1171874999986995819, 0.1210937499986559779, 0.1249999999986123878, 0.1562499999982641941, 0.1718749999980896670, 0.1796874999980059007, 0.1835937499979638510, 0.1855468749979440057, 0.1865234374979332643, 0.1874999999979225507, 0.2187499999978837206, 0.2343749999978601839, 0.2421874999978483878, 0.2460937499978433918, 0.2480468749978424203, 0.2499999999978414489, 0.2812499999978634313, 0.2968749999978704257, 0.3046874999978750886, 0.3085937499978803067, 0.3124999999978855247, 0.3437499999979258813, 0.3593749999979464760, 0.3671874999979566345, 0.3749999999979667931, 0.4999999999981064036, 0.5624999999981761256, 0.5937499999982130960, 0.6093749999982316368, 0.6171874999982408516, 0.6249999999982500665, 0.6562499999982865928, 0.6718749999983006926, 0.6796874999983039123, 0.6835937499983055776, 0.6874999999983072430, 0.7187499999982993604, 0.7343749999982969179, 0.7421874999982993604, 0.7460937499982994714, 0.7480468749983008037, 0.7499999999983021359, 0.7812499999983306687, 0.7968749999983447685, 0.8046874999983562038, 0.8085937499983619769, 0.8105468749983758547, 0.8115234374983829602, 0.8124999999983899546, 0.8437499999986364241, 0.8593749999987574384, 0.8671874999988179455, 0.8710937499988491428, 0.8749999999988802291, 0.9062499999991531219, 0.9218749999992918998, 0.9296874999993632871, 0.9374999999994347855, 1.000000000000000000 ),
 .UNSPECIFIED. ) ;
#18697=ADVANCED_FACE ( 'NONE', ( #15938 ), #14158, .T. ) ;
#18701=CARTESIAN_POINT ( 'NONE',  ( 7.552123853614987503, 35.83646061958899764, -141.8420144836698285 ) ) ;
#18704=AXIS2_PLACEMENT_3D ( 'NONE', #6055, #7715, #5931 ) ;
#18727=VERTEX_POINT ( 'NONE', #23433 ) ;
#18730=CARTESIAN_POINT ( 'NONE',  ( -30.50000000000000000, 47.50000000000000000, -149.0552959529999839 ) ) ;
#18731=CARTESIAN_POINT ( 'NONE',  ( -30.49999999990000177, 37.00000000000000000, -139.0552959529999839 ) ) ;
#18742=CARTESIAN_POINT ( 'NONE',  ( 8.500000000060001781, 38.50000000000000000, -144.0552959529999839 ) ) ;
#18746=CARTESIAN_POINT ( 'NONE',  ( 9.891652228665913427, 37.55988566378615445, -141.6187646494944659 ) ) ;
#18755=LINE ( 'NONE', #9922, #17791 ) ;
#18765=CARTESIAN_POINT ( 'NONE',  ( -46.50000000000000000, 37.00000000000000000, -149.0552959529999839 ) ) ;
#18772=CARTESIAN_POINT ( 'NONE',  ( 9.689837539793540344, 37.91893336569569328, -146.3818244917540312 ) ) ;
#18860=VECTOR ( 'NONE', #11293, 1000.000000000000000 ) ;
#18870=ORIENTED_EDGE ( 'NONE', *, *, #8082, .F. ) ;
#18924=ORIENTED_EDGE ( 'NONE', *, *, #5752, .T. ) ;
#18975=CARTESIAN_POINT ( 'NONE',  ( 7.051758037318819561, 36.60562334003225970, -146.5244709269151429 ) ) ;
#18979=AXIS2_PLACEMENT_3D ( 'NONE', #17259, #13687, #967 ) ;
#18995=DIRECTION ( 'NONE',  ( 1.000000000000000000, 2.602084747549999882E-17, 0.000000000000000000 ) ) ;
#19009=CARTESIAN_POINT ( 'NONE',  ( 9.168738215927051627, 38.34300703367464536, -146.1639638664460961 ) ) ;
#19020=CARTESIAN_POINT ( 'NONE',  ( -46.29070078880000239, 45.00000000000000000, -147.5552959540000018 ) ) ;
#19027=EDGE_LOOP ( 'NONE', ( #4500, #9340, #6775, #17196, #3376, #280, #19352, #16632 ) ) ;
#19038=VERTEX_POINT ( 'NONE', #17311 ) ;
#19041=PLANE ( 'NONE',  #20058 ) ;
#19069=VECTOR ( 'NONE', #22051, 1000.000000000000000 ) ;
#19096=CARTESIAN_POINT ( 'NONE',  ( 8.500000000060001781, 35.50000000000000000, -146.0552959529999839 ) ) ;
#19110=FACE_OUTER_BOUND ( 'NONE', #4978, .T. ) ;
#19129=LINE ( 'NONE', #14223, #18509 ) ;
#19158=CYLINDRICAL_SURFACE ( 'NONE', #6742, 1.500000000000001332 ) ;
#19216=DIRECTION ( 'NONE',  ( 1.000000000000000000, 0.000000000000000000, -2.257171095940000041E-12 ) ) ;
#19245=ORIENTED_EDGE ( 'NONE', *, *, #16286, .T. ) ;
#19263=ORIENTED_EDGE ( 'NONE', *, *, #14913, .T. ) ;
#19265=EDGE_CURVE ( 'NONE', #19696, #4078, #3976, .T. ) ;
#19276=EDGE_LOOP ( 'NONE', ( #1663, #7078, #5869, #16144, #17129, #23036, #9201 ) ) ;
#19300=CARTESIAN_POINT ( 'NONE',  ( 8.500000000060001781, 35.50000000000000000, -144.0552959529999839 ) ) ;
#19308=CARTESIAN_POINT ( 'NONE',  ( 8.250850001128238631, 38.47921821292768385, -142.0398975025202333 ) ) ;
#19312=CARTESIAN_POINT ( 'NONE',  ( -45.83792946319999828, 45.00000000000000000, -146.9594324700000243 ) ) ;
#19314=VERTEX_POINT ( 'NONE', #13012 ) ;
#19352=ORIENTED_EDGE ( 'NONE', *, *, #21701, .T. ) ;
#19507=ORIENTED_EDGE ( 'NONE', *, *, #551, .F. ) ;
#19513=DIRECTION ( 'NONE',  ( -1.000000000000000000, 0.000000000000000000, 2.257221436789999912E-12 ) ) ;
#19541=DIRECTION ( 'NONE',  ( 2.602084747549999882E-17, -1.000000000000000000, -5.873289694040000105E-29 ) ) ;
#19549=CARTESIAN_POINT ( 'NONE',  ( 7.098883623607016524, 36.46423812985609203, -141.6133621761054826 ) ) ;
#19565=FACE_OUTER_BOUND ( 'NONE', #11586, .T. ) ;
#19587=LINE ( 'NONE', #21495, #15593 ) ;
#19596=DIRECTION ( 'NONE',  ( -1.000000000000000000, 0.000000000000000000, 2.257171095940000041E-12 ) ) ;
#19599=CARTESIAN_POINT ( 'NONE',  ( 9.225170223517482171, 35.68671641322836052, -141.9279471768529390 ) ) ;
#19607=CARTESIAN_POINT ( 'NONE',  ( -32.99999999989999822, 37.00000000000000000, -138.5552959529999839 ) ) ;
#19642=DIRECTION ( 'NONE',  ( 0.000000000000000000, -1.000000000000000000, 0.000000000000000000 ) ) ;
#19661=CARTESIAN_POINT ( 'NONE',  ( 7.108347771513900071, 36.44011433609385620, -141.6187646495017702 ) ) ;
#19685=CARTESIAN_POINT ( 'NONE',  ( -34.61111111099999960, 26.50000000000000000, -140.5552959529999839 ) ) ;
#19696=VERTEX_POINT ( 'NONE', #11768 ) ;
#19714=CARTESIAN_POINT ( 'NONE',  ( 9.161058160660402905, 35.65265274061410139, -141.9492515423469285 ) ) ;
#19719=ORIENTED_EDGE ( 'NONE', *, *, #13432, .F. ) ;
#19729=EDGE_LOOP ( 'NONE', ( #7361, #10928, #18924, #2721, #7021, #4847, #10910, #7609, #20353, #6308, #14234, #8466 ) ) ;
#19754=VECTOR ( 'NONE', #1298, 1000.000000000000000 ) ;
#19783=VERTEX_POINT ( 'NONE', #1796 ) ;
#19788=CARTESIAN_POINT ( 'NONE',  ( 7.151459560400827087, 37.65757145640934311, -141.6431750412416193 ) ) ;
#19838=CARTESIAN_POINT ( 'NONE',  ( 8.997695683344982598, 35.58457175570028852, -141.9945801902854328 ) ) ;
#19850=CARTESIAN_POINT ( 'NONE',  ( -10.49999999989999822, 34.50000000000000000, -144.0552959529999839 ) ) ;
#19887=CARTESIAN_POINT ( 'NONE',  ( 14.50000000010000001, 37.00000000000000000, -144.0552959529999839 ) ) ;
#19903=CARTESIAN_POINT ( 'NONE',  ( 7.448738598091634522, 38.06998855381485924, -141.7958383015206891 ) ) ;
#19950=CARTESIAN_POINT ( 'NONE',  ( 8.749149998575488141, 35.52078178699984790, -142.0398975025203470 ) ) ;
#19996=VECTOR ( 'NONE', #12743, 1000.000000000000000 ) ;
#20016=MANIFOLD_SOLID_BREP ( 'lock_assembly.1\\Product1.1\\PIN.1\\PartBody', #14115 ) ;
#20018=CARTESIAN_POINT ( 'NONE',  ( 7.261465936361774176, 37.84621284174770039, -141.7028596377083147 ) ) ;
#20051=ADVANCED_FACE ( 'NONE', ( #23530 ), #3658, .F. ) ;
#20058=AXIS2_PLACEMENT_3D ( 'NONE', #10094, #13558, #17370 ) ;
#20067=CARTESIAN_POINT ( 'NONE',  ( 9.543956954615813615, 35.92288351715210126, -141.7992203786431276 ) ) ;
#20077=ADVANCED_FACE ( 'NONE', ( #6988 ), #10773, .T. ) ;
#20098=CARTESIAN_POINT ( 'NONE',  ( 8.697346895277828338, 35.50958615751394376, -146.0625927866750260 ) ) ;
#20112=DIRECTION ( 'NONE',  ( 0.000000000000000000, 1.000000000000000000, 0.000000000000000000 ) ) ;
#20128=VERTEX_POINT ( 'NONE', #17700 ) ;
#20134=VECTOR ( 'NONE', #7917, 1000.000000000000000 ) ;
#20194=CARTESIAN_POINT ( 'NONE',  ( 9.901116376611746261, 37.53576186991580954, -141.6133621760922665 ) ) ;
#20220=ORIENTED_EDGE ( 'NONE', *, *, #6764, .F. ) ;
#20269=STYLED_ITEM ( 'NONE', ( #1067 ), #22005 ) ;
#20281=ADVANCED_FACE ( 'NONE', ( #17433 ), #22441, .T. ) ;
#20292=EDGE_CURVE ( 'NONE', #11665, #10060, #18755, .T. ) ;
#20302=CARTESIAN_POINT ( 'NONE',  ( -44.50000000000000000, 45.00000000000000000, -148.4460207619999892 ) ) ;
#20311=ORIENTED_EDGE ( 'NONE', *, *, #6723, .T. ) ;
#20353=ORIENTED_EDGE ( 'NONE', *, *, #13432, .T. ) ;
#20366=CARTESIAN_POINT ( 'NONE',  ( 7.423740471920396544, 35.95513021493444228, -141.7841118834000440 ) ) ;
#20414=CARTESIAN_POINT ( 'NONE',  ( 9.749519600121018925, 37.82990536602501663, -141.6970570770093047 ) ) ;
#20470=VECTOR ( 'NONE', #16073, 1000.000000000000000 ) ;
#20533=CARTESIAN_POINT ( 'NONE',  ( 9.649788648777766653, 37.96362004170691762, -141.7484567676849281 ) ) ;
#20562=CARTESIAN_POINT ( 'NONE',  ( 9.843499027571208870, 37.67425020617515941, -146.4644491674870324 ) ) ;
#20575=LINE ( 'NONE', #2731, #15 ) ;
#20602=CARTESIAN_POINT ( 'NONE',  ( 7.366555212978977529, 36.01714620922514598, -141.7565619021944485 ) ) ;
#20617=ADVANCED_FACE ( 'NONE', ( #8206 ), #15717, .T. ) ;
#20651=CARTESIAN_POINT ( 'NONE',  ( 9.291372094100973200, 38.27544467346150014, -141.9048323916335050 ) ) ;
#20673=CARTESIAN_POINT ( 'NONE',  ( -30.49999999990000177, 26.50000000000000000, -140.5552959529999839 ) ) ;
#20677=DIRECTION ( 'NONE',  ( 1.000000000000000000, 0.000000000000000000, 0.000000000000000000 ) ) ;
#20687=CARTESIAN_POINT ( 'NONE',  ( -31.00000000000000000, 37.00000000000000000, -149.5552959529999839 ) ) ;
#20760=FACE_OUTER_BOUND ( 'NONE', #2779, .T. ) ;
#20767=CARTESIAN_POINT ( 'NONE',  ( 7.940121941277687334, 38.39185605419793035, -146.1320387297646448 ) ) ;
#20789=CARTESIAN_POINT ( 'NONE',  ( -30.49999999990000177, 26.50000000000000000, -139.0552959529999839 ) ) ;
#20795=CARTESIAN_POINT ( 'NONE',  ( 9.861913442962562115, 36.36936048521160103, -146.4749235844630846 ) ) ;
#20801=DIRECTION ( 'NONE',  ( 1.000000000000000000, 0.000000000000000000, -2.275957200481568888E-12 ) ) ;
#20804=( NAMED_UNIT ( * ) SI_UNIT ( $, .STERADIAN. ) SOLID_ANGLE_UNIT ( ) );
#20809=EDGE_LOOP ( 'NONE', ( #2116, #19507, #14140, #18510 ) ) ;
#20846=EDGE_CURVE ( 'NONE', #6638, #11714, #8793, .T. ) ;
#20890=CARTESIAN_POINT ( 'NONE',  ( 8.037076569876626664, 38.42714480829248913, -146.1079377423441201 ) ) ;
#20893=APPLICATION_CONTEXT ( 'automotive_design' ) ;
#20908=CARTESIAN_POINT ( 'NONE',  ( -30.49999999990000177, 34.50000000000000000, -144.0552959529999839 ) ) ;
#20917=CIRCLE ( 'NONE', #17872, 0.5000000000000004441 ) ;
#20923=CARTESIAN_POINT ( 'NONE',  ( 9.253750895402886201, 35.69920382850602891, -146.1911047861467807 ) ) ;
#20965=LINE ( 'NONE', #15251, #22490 ) ;
#20972=DIRECTION ( 'NONE',  ( -1.000000000000000000, 1.734728570689999873E-18, 2.257171095940000041E-12 ) ) ;
#21009=CARTESIAN_POINT ( 'NONE',  ( 7.587328409695290432, 38.19466532143988502, -146.2522312777784634 ) ) ;
#21018=DIRECTION ( 'NONE',  ( 2.257171095940000041E-12, 1.003664318210000046E-28, 1.000000000000000000 ) ) ;
#21057=SURFACE_STYLE_FILL_AREA ( #15807 ) ;
#21063=LINE ( 'NONE', #17245, #4184 ) ;
#21104=CARTESIAN_POINT ( 'NONE',  ( 8.288471959293929103, 38.48538972801363656, -142.0444128376232129 ) ) ;
#21122=VECTOR ( 'NONE', #4820, 1000.000000000000000 ) ;
#21162=ORIENTED_EDGE ( 'NONE', *, *, #18288, .T. ) ;
#21176=( NAMED_UNIT ( * ) SI_UNIT ( $, .STERADIAN. ) SOLID_ANGLE_UNIT ( ) );
#21200=CARTESIAN_POINT ( 'NONE',  ( -35.73252798949999942, 37.00000000000000000, -140.5552959529999839 ) ) ;
#21205=COLOUR_RGB ( '', 0.08235294, 0.09019608, 0.10196078) ;
#21289=VERTEX_POINT ( 'NONE', #2811 ) ;
#21315=CARTESIAN_POINT ( 'NONE',  ( -38.72222222220000276, 26.50000000000000000, -140.5552959529999839 ) ) ;
#21340=CARTESIAN_POINT ( 'NONE',  ( -10.49999999989999822, 37.00000000000000000, -144.0552959529999839 ) ) ;
#21341=CARTESIAN_POINT ( 'NONE',  ( 7.672998245282296459, 38.25143462710926912, -141.8910607812413502 ) ) ;
#21347=EDGE_CURVE ( 'NONE', #15836, #19038, #8689, .T. ) ;
#21348=CARTESIAN_POINT ( 'NONE',  ( -46.50000000000000000, 47.50000000000000000, -149.0552959529999839 ) ) ;
#21379=VECTOR ( 'NONE', #22454, 1000.000000000000000 ) ;
#21393=CARTESIAN_POINT ( 'NONE',  ( 9.771538001791512329, 36.20254759283128010, -141.6854458089526645 ) ) ;
#21405=CARTESIAN_POINT ( 'NONE',  ( 8.500000000060001781, 38.50000000000000000, -146.0552959529999839 ) ) ;
#21438=PLANE ( 'NONE',  #2274 ) ;
#21455=CARTESIAN_POINT ( 'NONE',  ( 7.250480400028753714, 36.17009463394629876, -141.6970570770266136 ) ) ;
#21472=LINE ( 'NONE', #5401, #11009 ) ;
#21495=CARTESIAN_POINT ( 'NONE',  ( -38.39535039420000118, 26.50000000000000000, -147.5552959529999839 ) ) ;
#21507=CARTESIAN_POINT ( 'NONE',  ( 9.371776569741914642, 35.77840329725038515, -141.8736084709495060 ) ) ;
#21515=VERTEX_POINT ( 'NONE', #15385 ) ;
#21574=CARTESIAN_POINT ( 'NONE',  ( 8.037995166842678785, 38.42729146114034933, -142.0027968016258342 ) ) ;
#21580=CARTESIAN_POINT ( 'NONE',  ( -46.00000000000000000, 37.00000000000000000, -149.0552959529999839 ) ) ;
#21592=EDGE_CURVE ( 'NONE', #10616, #8910, #18658, .T. ) ;
#21628=CARTESIAN_POINT ( 'NONE',  ( 9.863231070447312732, 36.37411343960744148, -141.6348998444321410 ) ) ;
#21638=DIRECTION ( 'NONE',  ( 2.602084747549999882E-17, -1.000000000000000000, -5.873289694040000105E-29 ) ) ;
#21640=LINE ( 'NONE', #19850, #17563 ) ;
#21667=EDGE_LOOP ( 'NONE', ( #7119, #22194, #16159, #11221 ) ) ;
#21696=DIRECTION ( 'NONE',  ( -1.000000000000000000, 1.734728570689999873E-18, 2.257171095940000041E-12 ) ) ;
#21697=CARTESIAN_POINT ( 'NONE',  ( 7.682970039224882086, 38.25799164440910971, -141.8948580842254614 ) ) ;
#21701=EDGE_CURVE ( 'NONE', #13387, #14263, #4545, .T. ) ;
#21710=LINE ( 'NONE', #5395, #14898 ) ;
#21721=DIRECTION ( 'NONE',  ( -1.000000000000000000, 0.000000000000000000, 2.257076750570000197E-12 ) ) ;
#21748=CARTESIAN_POINT ( 'NONE',  ( 8.711528040173069698, 35.51461027188803143, -142.0444128376234687 ) ) ;
#21751=DIRECTION ( 'NONE',  ( -1.000000000000000000, 0.000000000000000000, 2.258108725280000263E-12 ) ) ;
#21779=EDGE_LOOP ( 'NONE', ( #18324, #14008, #4018, #23041 ) ) ;
#21793=CARTESIAN_POINT ( 'NONE',  ( -30.49999999990000177, 26.50000000000000000, -140.5552959529999839 ) ) ;
#21805=LINE ( 'NONE', #18183, #16702 ) ;
#21815=CARTESIAN_POINT ( 'NONE',  ( 7.922905632975483670, 38.38455376863645085, -141.9737733526858960 ) ) ;
#21839=AXIS2_PLACEMENT_3D ( 'NONE', #14206, #1257, #1483 ) ;
#21847=UNCERTAINTY_MEASURE_WITH_UNIT (LENGTH_MEASURE( 1.000000000000000082E-05 ), #15219, 'distance_accuracy_value', 'NONE');
#21863=CARTESIAN_POINT ( 'NONE',  ( 9.334143923700091605, 35.75332166666289879, -141.8883195129358228 ) ) ;
#21949=VECTOR ( 'NONE', #9420, 1000.000000000000000 ) ;
#21966=CARTESIAN_POINT ( 'NONE',  ( -31.00000000000000000, 47.50000000000000000, -149.0552959529999839 ) ) ;
#21969=CARTESIAN_POINT ( 'NONE',  ( 9.563783796762269418, 38.05753333485859002, -141.7899860742832061 ) ) ;
#21975=MECHANICAL_DESIGN_GEOMETRIC_PRESENTATION_REPRESENTATION('',(#2228),#17419);
#21976=VERTEX_POINT ( 'NONE', #7708 ) ;
#22000=CARTESIAN_POINT ( 'NONE',  ( 9.059878058829383463, 35.60814394579439579, -146.1320387297621153 ) ) ;
#22005=ADVANCED_BREP_SHAPE_REPRESENTATION ( '', ( #20016, #5025 ), #7334 ) ;
#22034=ADVANCED_FACE ( 'NONE', ( #2952 ), #2726, .T. ) ;
#22040=CARTESIAN_POINT ( 'NONE',  ( 8.401454119002149667, 35.50000000000029843, -142.0552959529997850 ) ) ;
#22051=DIRECTION ( 'NONE',  ( 0.000000000000000000, -1.000000000000000000, 0.000000000000000000 ) ) ;
#22087=CARTESIAN_POINT ( 'NONE',  ( 9.338338750285297252, 38.24386024261577433, -141.8866982261258727 ) ) ;
#22121=ORIENTED_EDGE ( 'NONE', *, *, #20292, .T. ) ;
#22153=CARTESIAN_POINT ( 'NONE',  ( 7.753210631989132295, 35.69821382032984047, -141.9207453427739267 ) ) ;
#22171=ORIENTED_EDGE ( 'NONE', *, *, #6823, .F. ) ;
#22194=ORIENTED_EDGE ( 'NONE', *, *, #19265, .F. ) ;
#22203=CARTESIAN_POINT ( 'NONE',  ( 9.499215171620216225, 38.12188228892512853, -141.8201969984096422 ) ) ;
#22229=DIRECTION ( 'NONE',  ( -2.257157423930000049E-12, 0.000000000000000000, -1.000000000000000000 ) ) ;
#22258=PLANE ( 'NONE',  #15141 ) ;
#22264=CARTESIAN_POINT ( 'NONE',  ( 8.300958730110608030, 35.50974402357368831, -142.0478759868927057 ) ) ;
#22311=CARTESIAN_POINT ( 'NONE',  ( 8.985684983851607299, 38.42005234198289543, -141.9976801200056968 ) ) ;
#22323=ORIENTED_EDGE ( 'NONE', *, *, #15989, .T. ) ;
#22343=CARTESIAN_POINT ( 'NONE',  ( -46.29070078859999882, 27.75000000000000000, -147.5552959529999839 ) ) ;
#22356=DIRECTION ( 'NONE',  ( -1.000000000000000000, 0.000000000000000000, 2.256683728769999802E-12 ) ) ;
#22358=ORIENTED_EDGE ( 'NONE', *, *, #15490, .F. ) ;
#22372=VECTOR ( 'NONE', #19513, 1000.000000000000000 ) ;
#22390=CIRCLE ( 'NONE', #5663, 0.5000000000000004441 ) ;
#22431=CARTESIAN_POINT ( 'NONE',  ( 9.926991605570590238, 37.46297533359125964, -141.5985056068803942 ) ) ;
#22441=PLANE ( 'NONE',  #3735 ) ;
#22454=DIRECTION ( 'NONE',  ( 2.256988247090000272E-12, 0.000000000000000000, 1.000000000000000000 ) ) ;
#22475=LINE ( 'NONE', #20687, #14817 ) ;
#22490=VECTOR ( 'NONE', #2641, 1000.000000000000000 ) ;
#22492=AXIS2_PLACEMENT_3D ( 'NONE', #10728, #1723, #18246 ) ;
#22522=DIRECTION ( 'NONE',  ( 1.000000000000000000, 0.000000000000000000, 0.000000000000000000 ) ) ;
#22531=DIRECTION ( 'NONE',  ( 2.602084747549999882E-17, -1.000000000000000000, -5.873289694040000105E-29 ) ) ;
#22539=ORIENTED_EDGE ( 'NONE', *, *, #18484, .F. ) ;
#22612=CARTESIAN_POINT ( 'NONE',  ( 8.500000000060001781, 37.00000000000000000, -144.0552959529999839 ) ) ;
#22624=ADVANCED_FACE ( 'NONE', ( #16217 ), #14663, .T. ) ;
#22633=DIRECTION ( 'NONE',  ( 1.000000000000000000, 0.000000000000000000, 0.000000000000000000 ) ) ;
#22669=ORIENTED_EDGE ( 'NONE', *, *, #6232, .F. ) ;
#22716=VERTEX_POINT ( 'NONE', #3956 ) ;
#22722=CARTESIAN_POINT ( 'NONE',  ( 14.50000000010000001, 34.50000000000000000, -144.0552959529999839 ) ) ;
#22730=CIRCLE ( 'NONE', #9797, 2.000000000000001776 ) ;
#22787=VECTOR ( 'NONE', #1403, 1000.000000000000000 ) ;
#22795=VECTOR ( 'NONE', #17730, 1000.000000000000000 ) ;
#22844=EDGE_CURVE ( 'NONE', #11330, #18727, #20965, .T. ) ;
#22892=CARTESIAN_POINT ( 'NONE',  ( 8.401003265635759831, 38.49757205280096173, -142.0534435078293711 ) ) ;
#22911=CARTESIAN_POINT ( 'NONE',  ( 7.831261784188757957, 35.65699296629090753, -146.1639638664211418 ) ) ;
#22932=EDGE_CURVE ( 'NONE', #9140, #896, #13355, .T. ) ;
#22942=VERTEX_POINT ( 'NONE', #12253 ) ;
#22952=CARTESIAN_POINT ( 'NONE',  ( 8.400763094363121297, 38.49996446091597591, -146.0553226073556914 ) ) ;
#22961=B_SPLINE_CURVE_WITH_KNOTS ( 'NONE', 3,
 ( #17691, #3535, #18164, #1877, #21748, #19950, #14595, #16265, #3650, #12560, #5547, #19838, #9101, #16384, #23401, #15899, #12439, #19714, #19599, #14358, #5437, #1759, #7333, #91, #8981, #21863, #12794, #5079, #21507, #23521, #14482, #1528, #7218, #12681, #23289, #20067, #17805, #3764, #8624, #3294, #8749, #1399, #23165, #6860, #10652, #14125, #1648, #21393, #12323, #8869, #10526, #21628, #16028, #6981, #14243, #5190, #16147, #3996, #11228, #2001, #22431, #18395, #20194, #18746, #311, #18502, #9441, #2221, #12911, #5887, #433, #20414, #7671, #15172, #2456, #20533, #16719, #6004, #2344, #5655, #15051, #21969, #14941, #22203, #13144, #16841, #11468, #4106, #6127, #9678, #13258, #22087, #7786, #16954, #20651, #9568, #11344, #7552, #4233, #11007, #13383, #553, #18629, #22311, #660, #3890, #7893, #5775, #2104, #18290, #9221, #16489 ),
 .UNSPECIFIED., .F., .F.,
 ( 4, 2, 1, 2, 2, 2, 1, 1, 2, 2, 2, 2, 1, 1, 1, 2, 2, 2, 2, 2, 1, 2, 2, 2, 2, 1, 2, 2, 2, 1, 2, 2, 2, 2, 2, 1, 2, 2, 2, 1, 1, 2, 2, 2, 2, 1, 1, 2, 2, 2, 2, 1, 1, 1, 2, 2, 2, 1, 1, 2, 2, 2, 1, 2, 2, 4 ),
 ( 0.000000000000000000, 0.03125000000007426698, 0.04687500000011055046, 0.05468750000012817525, 0.06250000000014580004, 0.09375000000021557756, 0.1093750000002510908, 0.1171875000002707279, 0.1210937500002829403, 0.1250000000002951528, 0.1562500000004152234, 0.1718750000004748146, 0.1796875000005022649, 0.1835937500005136447, 0.1855468750005199452, 0.1865234375005227485, 0.1875000000005255518, 0.2187500000006049050, 0.2343750000006437628, 0.2421875000006631917, 0.2460937500006700751, 0.2480468750006724898, 0.2500000000006749046, 0.2812500000006796230, 0.2968750000006838974, 0.3046875000006860068, 0.3085937500006871170, 0.3125000000006881717, 0.3437500000006842860, 0.3593750000006820100, 0.3671875000006808443, 0.3750000000006796785, 0.5000000000007456258, 0.5625000000007787104, 0.5937500000007961409, 0.6093750000008081313, 0.6171875000008142376, 0.6250000000008202328, 0.6562500000008438805, 0.6718750000008558709, 0.6796875000008618661, 0.6835937500008635315, 0.6875000000008651968, 0.7187500000009028334, 0.7343750000009242607, 0.7421875000009376944, 0.7460937500009454659, 0.7480468750009519052, 0.7500000000009582335, 0.7812500000010785817, 0.7968750000011431966, 0.8046875000011735057, 0.8085937500011912693, 0.8105468750012013723, 0.8115234375011972645, 0.8125000000011932677, 0.8437500000010063061, 0.8593750000009123813, 0.8671875000008619772, 0.8710937500008353318, 0.8750000000008085754, 0.9062500000006017409, 0.9218750000005005996, 0.9296875000004484191, 0.9375000000003962386, 1.000000000000000000 ),
 .UNSPECIFIED. ) ;
#22998=CARTESIAN_POINT ( 'NONE',  ( 8.212030648970713997, 38.47214394625672185, -142.0347430633063937 ) ) ;
#23036=ORIENTED_EDGE ( 'NONE', *, *, #18009, .F. ) ;
#23041=ORIENTED_EDGE ( 'NONE', *, *, #14437, .T. ) ;
#23111=DIRECTION ( 'NONE',  ( -1.000000000000000000, 0.000000000000000000, 2.257221436789999912E-12 ) ) ;
#23115=FACE_BOUND ( 'NONE', #2097, .T. ) ;
#23116=CARTESIAN_POINT ( 'NONE',  ( 7.286767612010325301, 37.88214748707077462, -141.7161147874617768 ) ) ;
#23119=DIRECTION ( 'NONE',  ( -2.257171095940000041E-12, 0.000000000000000000, -1.000000000000000000 ) ) ;
#23132=CARTESIAN_POINT ( 'NONE',  ( 8.500000000060001781, 37.00000000000000000, -144.0552959529999839 ) ) ;
#23138=CIRCLE ( 'NONE', #6019, 2.500000000000002220 ) ;
#23165=CARTESIAN_POINT ( 'NONE',  ( 9.713232388825044694, 36.11785251390046625, -141.7161147870856155 ) ) ;
#23177=VERTEX_POINT ( 'NONE', #11275 ) ;
#23195=ADVANCED_FACE ( 'NONE', ( #7377 ), #3929, .T. ) ;
#23234=CARTESIAN_POINT ( 'NONE',  ( 7.232790317618205123, 36.19721093022112512, -141.6876531320059200 ) ) ;
#23289=CARTESIAN_POINT ( 'NONE',  ( 9.533096737499036522, 35.91239492147925461, -141.8042231713539536 ) ) ;
#23296=FACE_OUTER_BOUND ( 'NONE', #19276, .T. ) ;
#23311=CYLINDRICAL_SURFACE ( 'NONE', #4142, 0.5000000000000004441 ) ;
#23331=VERTEX_POINT ( 'NONE', #19020 ) ;
#23342=DIRECTION ( 'NONE',  ( 1.000000000000000000, 0.000000000000000000, 0.000000000000000000 ) ) ;
#23351=CARTESIAN_POINT ( 'NONE',  ( 7.838941837282176195, 38.34734725831290802, -141.9492515416635001 ) ) ;
#23401=CARTESIAN_POINT ( 'NONE',  ( 9.069815628852895273, 35.61242929765868581, -141.9757830863595700 ) ) ;
#23419=ORIENTED_EDGE ( 'NONE', *, *, #14913, .F. ) ;
#23427=CARTESIAN_POINT ( 'NONE',  ( 14.50000000010000001, 37.00000000000000000, -144.0552959529999839 ) ) ;
#23433=CARTESIAN_POINT ( 'NONE',  ( -30.50000000000000000, 26.50000000000000000, -149.0552959529999839 ) ) ;
#23464=CARTESIAN_POINT ( 'NONE',  ( 8.002304315546503233, 38.41542824385604149, -141.9945801900086622 ) ) ;
#23470=DIRECTION ( 'NONE',  ( 2.602084747549999882E-17, -1.000000000000000000, -5.873289694040000105E-29 ) ) ;
#23472=ORIENTED_EDGE ( 'NONE', *, *, #8469, .F. ) ;
#23496=EDGE_CURVE ( 'NONE', #18574, #9140, #21640, .T. ) ;
#23500=AXIS2_PLACEMENT_3D ( 'NONE', #12147, #19541, #15730 ) ;
#23519=EDGE_CURVE ( 'NONE', #18727, #6756, #11952, .T. ) ;
#23521=CARTESIAN_POINT ( 'NONE',  ( 9.428880901062701270, 35.82197050348334955, -141.8499009806686786 ) ) ;
#23530=FACE_OUTER_BOUND ( 'NONE', #17765, .T. ) ;
#23538=VECTOR ( 'NONE', #9597, 1000.000000000000000 ) ;
ENDSEC;
END-ISO-10303-21;
